ISO-10303-21;
HEADER;
FILE_DESCRIPTION (('STEP AP214'),
    '1' );
FILE_NAME ('Catch Spring.step',
    '2026-10-06T09:00:30',
    ( '' ),
    ( '' ),
    'SwSTEP 2.0',
    'SolidWorks 2020',
    '' );
FILE_SCHEMA (( 'AUTOMOTIVE_DESIGN' ));
ENDSEC;

DATA;
#14=CARTESIAN_POINT ( 'NONE',  ( 3.314820598666778917, -5.455691467570147779, -47.04669147682499641 ) ) ;
#89=CARTESIAN_POINT ( 'NONE',  ( -4.778993077004805912, -1.464489131705188019, -68.10000000002500542 ) ) ;
#96=CARTESIAN_POINT ( 'NONE',  ( 0.2945360517547964130, 4.690762039826936736, -70.15875473022499875 ) ) ;
#100=CARTESIAN_POINT ( 'NONE',  ( 2.776548632478545553, -3.583402058917904753, -52.50430438132499233 ) ) ;
#131=CARTESIAN_POINT ( 'NONE',  ( -5.110483438867316153, -2.062468175234513534, -60.18491726642499628 ) ) ;
#146=CARTESIAN_POINT ( 'NONE',  ( -0.9130200810698786418, -4.996423850591022564, -44.10000000002499121 ) ) ;
#165=CARTESIAN_POINT ( 'NONE',  ( 3.314820598666778917, -5.455691467570147779, -46.56669147682499954 ) ) ;
#246=CARTESIAN_POINT ( 'NONE',  ( -4.889194147463507001, -0.6752612934842897596, -68.10000000002499121 ) ) ;
#251=CARTESIAN_POINT ( 'NONE',  ( -4.287590041606510916, 1.413705153860731034, -68.74019511502500279 ) ) ;
#258=CARTESIAN_POINT ( 'NONE',  ( 4.545032752014871669, -0.3361547907463971474, -49.12442242802499237 ) ) ;
#278=STYLED_ITEM ( 'NONE', ( #27092 ), #24185 ) ;
#293=CARTESIAN_POINT ( 'NONE',  ( -0.06606756225350368661, 5.646037861211643083, -57.79818518972499675 ) ) ;
#308=CARTESIAN_POINT ( 'NONE',  ( 0.7512103448916097603, -4.944508214582001848, -44.10000000002501253 ) ) ;
#315=CARTESIAN_POINT ( 'NONE',  ( 2.295476649252899293, -3.592865671589305698, -43.56966640442499994 ) ) ;
#327=CARTESIAN_POINT ( 'NONE',  ( -3.250950776947242993, -3.159825117472811140, -47.60083066912499561 ) ) ;
#366=CARTESIAN_POINT ( 'NONE',  ( -3.642744778375347270, -3.605832648298818111, -44.10000000002499121 ) ) ;
#395=CARTESIAN_POINT ( 'NONE',  ( -3.985743628842677300, -2.180176701716181942, -52.94982952342499516 ) ) ;
#398=CARTESIAN_POINT ( 'NONE',  ( 1.060425485998340633, -4.855416528021975431, -68.10000000002500542 ) ) ;
#408=CARTESIAN_POINT ( 'NONE',  ( -0.8929276208064895748, -4.785132802852544387, -68.65745670422501234 ) ) ;
#413=CARTESIAN_POINT ( 'NONE',  ( -4.543473910928012671, 0.02303893552233621245, -62.57122063472500884 ) ) ;
#447=CARTESIAN_POINT ( 'NONE',  ( 4.569612387855602087, -0.08076758077263379576, -58.09793411332499602 ) ) ;
#463=CARTESIAN_POINT ( 'NONE',  ( 2.806119477842475618, -3.711775362531495759, -44.10000000002499121 ) ) ;
#472=CARTESIAN_POINT ( 'NONE',  ( -4.848570193085772750, 0.4842359979205512754, -47.22737393802500350 ) ) ;
#483=CARTESIAN_POINT ( 'NONE',  ( 2.137930486642451555, 6.059703978454344941, -45.49079303332499791 ) ) ;
#523=CARTESIAN_POINT ( 'NONE',  ( -2.744417411265728912, -4.298957096598221561, -44.10000000002499121 ) ) ;
#554=CARTESIAN_POINT ( 'NONE',  ( 4.692739937114380311, 0.5303478879429834869, -55.01771407622499765 ) ) ;
#557=CARTESIAN_POINT ( 'NONE',  ( -4.646218698937943259, 0.8004880362142797745, -68.10000000002497700 ) ) ;
#592=CARTESIAN_POINT ( 'NONE',  ( 1.128437890537931976, -3.898078178863690901, -68.10000000002501963 ) ) ;
#596=CARTESIAN_POINT ( 'NONE',  ( -0.8249440165340218289, 4.504533947698903695, -60.65324387862499833 ) ) ;
#612=CARTESIAN_POINT ( 'NONE',  ( 2.873326072151168642, -3.563018121669343063, -44.10000000002499831 ) ) ;
#620=( LENGTH_UNIT ( ) NAMED_UNIT ( * ) SI_UNIT ( .MILLI., .METRE. ) );
#622=CARTESIAN_POINT ( 'NONE',  ( -0.5163256777700186984, 4.538631023554793309, -47.86410749632499773 ) ) ;
#636=CARTESIAN_POINT ( 'NONE',  ( -2.393684743089937061, 3.904820337558664978, -45.05531229042499319 ) ) ;
#702=CARTESIAN_POINT ( 'NONE',  ( 3.599561039400463347, 4.779710538180673041, -54.62619010302499589 ) ) ;
#705=CARTESIAN_POINT ( 'NONE',  ( -4.145494824737311568, 0.03818007883295551630, -68.10000000002501963 ) ) ;
#716=CARTESIAN_POINT ( 'NONE',  ( 1.415268835064556363, -5.780081730213937341, -64.22397119102500085 ) ) ;
#747=CARTESIAN_POINT ( 'NONE',  ( 1.008954696561116027, 5.412080152108726949, -64.22744533512499743 ) ) ;
#762=CARTESIAN_POINT ( 'NONE',  ( 2.591254417889934825, -3.476099799987327987, -44.10000000002499121 ) ) ;
#771=CARTESIAN_POINT ( 'NONE',  ( 4.647199600633202365, 1.656603404052558348, -45.17627377572499370 ) ) ;
#784=CARTESIAN_POINT ( 'NONE',  ( 3.346097069915054512, -4.318458891539398437, -53.30430438132499660 ) ) ;
#825=FILL_AREA_STYLE_COLOUR ( '', #13827 ) ;
#851=CARTESIAN_POINT ( 'NONE',  ( -5.035266659556940638, -1.323295706752037670, -55.65102360502499579 ) ) ;
#855=CARTESIAN_POINT ( 'NONE',  ( -4.557930684098742802, 0.9655407268836344592, -68.10000000002501963 ) ) ;
#864=CARTESIAN_POINT ( 'NONE',  ( 1.008954696561116027, 5.412080152108726949, -62.62744533512499601 ) ) ;
#893=CARTESIAN_POINT ( 'NONE',  ( -0.6145358956450698296, -3.890912529351672422, -68.10000000002501963 ) ) ;
#899=CARTESIAN_POINT ( 'NONE',  ( 2.840551633548176191, -3.955783487875848881, -62.27197827312499356 ) ) ;
#917=CARTESIAN_POINT ( 'NONE',  ( 1.979015836267390194, -4.452375488360101663, -44.10000000002499121 ) ) ;
#924=CARTESIAN_POINT ( 'NONE',  ( -1.909971040720825908, -5.612411004515823088, -46.51520033292499789 ) ) ;
#936=CARTESIAN_POINT ( 'NONE',  ( -5.473571180597741836, 3.247285761689575168, -51.31267869292499739 ) ) ;
#1005=CARTESIAN_POINT ( 'NONE',  ( -1.034595936873321076, -4.789217790999566127, -55.18033560642498969 ) ) ;
#1009=CARTESIAN_POINT ( 'NONE',  ( -4.561626939327173780, 0.9596751652757145035, -68.10000000002500542 ) ) ;
#1018=CARTESIAN_POINT ( 'NONE',  ( 1.094823181362614140, 5.872682718251108547, -62.94744533522500518 ) ) ;
#1044=DIRECTION ( 'NONE',  ( 0.000000000000000000, 0.000000000000000000, 1.000000000000000000 ) ) ;
#1047=CARTESIAN_POINT ( 'NONE',  ( -0.8884012486115674401, 4.851036559086118416, -61.00324387862499975 ) ) ;
#1063=CARTESIAN_POINT ( 'NONE',  ( 2.841665746808334170, -3.648605867525280821, -44.10000000002500542 ) ) ;
#1072=CARTESIAN_POINT ( 'NONE',  ( 5.643028086411650435, 2.011589847869324377, -45.44627377572500393 ) ) ;
#1082=CARTESIAN_POINT ( 'NONE',  ( 4.421972129926214023, 1.961202595004077232, -52.27998794302499164 ) ) ;
#1146=CARTESIAN_POINT ( 'NONE',  ( 3.312932182603874232, 3.356011527877053702, -57.70805965152499795 ) ) ;
#1154=CARTESIAN_POINT ( 'NONE',  ( -4.166989350266031344, 0.2041299532645725889, -68.10000000002500542 ) ) ;
#1156=EDGE_LOOP ( 'NONE', ( #4268, #11999, #26019, #12570 ) ) ;
#1164=CARTESIAN_POINT ( 'NONE',  ( -4.469650141049659631, 2.071768678095493588, -65.02526299422498823 ) ) ;
#1186=CARTESIAN_POINT ( 'NONE',  ( -0.06606756225350368661, 5.646037861211643083, -57.31818518972499277 ) ) ;
#1203=CARTESIAN_POINT ( 'NONE',  ( -3.750715812471464350, 4.529495762826656780, -63.79933298482499993 ) ) ;
#1227=CARTESIAN_POINT ( 'NONE',  ( 4.101176313917073379, -1.931410228222276038, -51.89872167392500302 ) ) ;
#1243=CARTESIAN_POINT ( 'NONE',  ( -4.185672079393978784, 2.483218523716627768, -50.83267869292499341 ) ) ;
#1310=CARTESIAN_POINT ( 'NONE',  ( -4.178199994060139311, -1.098053884355550069, -56.05102360502500858 ) ) ;
#1325=CARTESIAN_POINT ( 'NONE',  ( 1.415268835064556363, -5.780081730213937341, -64.70397119102500483 ) ) ;
#1344=CARTESIAN_POINT ( 'NONE',  ( 4.432674687120906398, 4.607520344841867121, -48.69426496242499525 ) ) ;
#1353=CARTESIAN_POINT ( 'NONE',  ( 1.503739165058197713, -3.819987766133262408, -68.10000000002500542 ) ) ;
#1356=CARTESIAN_POINT ( 'NONE',  ( -4.246782972018593227, 0.8972508281424985688, -44.10000000002499831 ) ) ;
#1360=CARTESIAN_POINT ( 'NONE',  ( 5.258991878263315378, 0.1257858540645254708, -64.81686508972499894 ) ) ;
#1386=CARTESIAN_POINT ( 'NONE',  ( -0.7556487780321456960, 4.453147011089717111, -50.85792092402500231 ) ) ;
#1397=CARTESIAN_POINT ( 'NONE',  ( -5.649653782182448403, -1.974543963569185046, -50.88743646232499884 ) ) ;
#1409=ADVANCED_FACE ( 'NONE', ( #1519 ), #10951, .F. ) ;
#1471=CARTESIAN_POINT ( 'NONE',  ( -1.157762119782732135, -5.359362766143966006, -55.13033560642499253 ) ) ;
#1473=VERTEX_POINT ( 'NONE', #3548 ) ;
#1506=CLOSED_SHELL ( 'NONE', ( #15794, #6412, #1752, #1409 ) ) ;
#1507=CARTESIAN_POINT ( 'NONE',  ( -5.212126283948660621, -2.851000302232811201, -53.34982952342500084 ) ) ;
#1514=EDGE_CURVE ( 'NONE', #5941, #3457, #12030, .T. ) ;
#1515=CARTESIAN_POINT ( 'NONE',  ( 2.341423236568627164, -3.556873072008999159, -68.10000000002500542 ) ) ;
#1518=CARTESIAN_POINT ( 'NONE',  ( -2.794029045709408354, -2.766466238262267119, -44.10000000002498410 ) ) ;
#1519=FACE_OUTER_BOUND ( 'NONE', #22369, .T. ) ;
#1521=CARTESIAN_POINT ( 'NONE',  ( -4.150389416700803302, 1.923785201099231790, -65.77526299422500244 ) ) ;
#1537=CARTESIAN_POINT ( 'NONE',  ( 0.4314002833255045632, -3.971307163432137077, -44.10000000002498410 ) ) ;
#1547=CARTESIAN_POINT ( 'NONE',  ( -4.320323480314926634, -1.509945384023519965, -50.00743646232500339 ) ) ;
#1558=CARTESIAN_POINT ( 'NONE',  ( -4.890954027203302523, -0.1236851485102684334, -54.30673954922499291 ) ) ;
#1594=CARTESIAN_POINT ( 'NONE',  ( 0.5498575204270217398, -4.501552459765377101, -43.78057807742499818 ) ) ;
#1622=CARTESIAN_POINT ( 'NONE',  ( 1.387947292976095426, 4.364053279572889465, -60.06492395752500357 ) ) ;
#1631=CARTESIAN_POINT ( 'NONE',  ( -3.842035491633269739, -1.137847961864614899, -68.10000000002500542 ) ) ;
#1641=CARTESIAN_POINT ( 'NONE',  ( -4.287590041606506475, 1.413705153860729924, -68.34019511502499711 ) ) ;
#1659=CARTESIAN_POINT ( 'NONE',  ( -4.251243323665415907, -4.132078999800212316, -47.20083066912499703 ) ) ;
#1665=CARTESIAN_POINT ( 'NONE',  ( 2.288615330823977168, -3.575176636938152352, -68.10000000002500542 ) ) ;
#1668=CARTESIAN_POINT ( 'NONE',  ( -4.184103756552774556, 0.3543491974005151812, -44.10000000002499121 ) ) ;
#1672=CARTESIAN_POINT ( 'NONE',  ( 4.434603606053169500, 2.142645224031550555, -67.60315453642500927 ) ) ;
#1697=CARTESIAN_POINT ( 'NONE',  ( 1.423503787547387933, 4.651298240777052229, -50.71125421252500587 ) ) ;
#1707=CARTESIAN_POINT ( 'NONE',  ( 2.964344385329936937, 3.936232207905868030, -55.37619010302499589 ) ) ;
#1752=ADVANCED_FACE ( 'NONE', ( #14018 ), #21373, .T. ) ;
#1782=CARTESIAN_POINT ( 'NONE',  ( 1.815007998551255941, 5.706838904126064094, -59.98492395752499817 ) ) ;
#1800=CARTESIAN_POINT ( 'NONE',  ( -4.155524648305278568, -2.455537445457761869, -68.32382590962500046 ) ) ;
#1819=CARTESIAN_POINT ( 'NONE',  ( -5.545418199629476241, -2.237997381628727300, -59.38491726642499202 ) ) ;
#1825=CARTESIAN_POINT ( 'NONE',  ( 2.188149499615938964, -3.610012245673223319, -68.10000000002503384 ) ) ;
#1830=CARTESIAN_POINT ( 'NONE',  ( 3.916181512753878824, -4.480608557854155904, -64.97605006312500109 ) ) ;
#1852=CARTESIAN_POINT ( 'NONE',  ( -5.206543681532186163, -1.819677770405741413, -49.60743646232500481 ) ) ;
#1861=CARTESIAN_POINT ( 'NONE',  ( -3.221934060409652023, 3.671197199744479001, -53.98587006832499924 ) ) ;
#1901=CARTESIAN_POINT ( 'NONE',  ( 3.001777156698443250, -4.698362801289899693, -43.56966640442499283 ) ) ;
#1934=CARTESIAN_POINT ( 'NONE',  ( -4.631110635561381805, 2.546857509239208728, -59.06908057272500656 ) ) ;
#1951=CARTESIAN_POINT ( 'NONE',  ( -1.595193757947241497, 6.212219048941578059, -66.20876360962500939 ) ) ;
#1981=CARTESIAN_POINT ( 'NONE',  ( 2.771604730552712947, -3.765259971643367010, -68.10000000002500542 ) ) ;
#1990=CARTESIAN_POINT ( 'NONE',  ( 6.385918709370476343, 0.1527399656023400998, -64.54686508972500292 ) ) ;
#2012=CARTESIAN_POINT ( 'NONE',  ( -5.939015604524707115, -0.1501891088408410790, -53.55673954922500002 ) ) ;
#2025=CARTESIAN_POINT ( 'NONE',  ( -1.256295066205788347, -5.815478746186413694, -56.41033560642500078 ) ) ;
#2047=CARTESIAN_POINT ( 'NONE',  ( 3.915051063684143795, -2.600456723069958453, -42.55875473022500444 ) ) ;
#2057=CARTESIAN_POINT ( 'NONE',  ( 2.766343654246206984, -4.329863758072034940, -44.36966640442500420 ) ) ;
#2084=STYLED_ITEM ( 'NONE', ( #22315 ), #21218 ) ;
#2089=CARTESIAN_POINT ( 'NONE',  ( -4.300317018729668206, 2.364939115720640750, -59.41908057272499377 ) ) ;
#2103=CARTESIAN_POINT ( 'NONE',  ( 0.2444022557069348567, 3.892334458579129297, -68.95875473022499591 ) ) ;
#2122=CARTESIAN_POINT ( 'NONE',  ( -1.277581537031662107, -5.235359937796273400, -67.93704710652501433 ) ) ;
#2131=CARTESIAN_POINT ( 'NONE',  ( -4.891993053148940618, -0.3028084928693625666, -68.10000000002500542 ) ) ;
#2135=CARTESIAN_POINT ( 'NONE',  ( -4.574578478894093081, -2.192947688770922277, -44.10000000002499121 ) ) ;
#2165=CARTESIAN_POINT ( 'NONE',  ( -1.293561172433232986, -6.216321778783836294, -52.44706695232499527 ) ) ;
#2174=CARTESIAN_POINT ( 'NONE',  ( 3.357378826396556271, -2.722208303779470651, -55.40923804942499942 ) ) ;
#2203=CARTESIAN_POINT ( 'NONE',  ( 0.7190444496271986008, -5.886645524271489904, -43.78057807742499818 ) ) ;
#2286=CARTESIAN_POINT ( 'NONE',  ( 6.385918709376013247, 0.1527399656106667725, -64.06686508972499894 ) ) ;
#2293=CARTESIAN_POINT ( 'NONE',  ( 0.5797420292678476805, -4.971399746194223646, -68.10000000002500542 ) ) ;
#2305=CARTESIAN_POINT ( 'NONE',  ( -0.8249440165340113928, 4.504533947698903695, -60.25324387862499975 ) ) ;
#2334=CARTESIAN_POINT ( 'NONE',  ( 4.332295931058598448, 4.388630459628991787, -58.18805965152500193 ) ) ;
#2359=CARTESIAN_POINT ( 'NONE',  ( 3.248659393266399409, -2.157825791482659294, -43.35875473022499449 ) ) ;
#2370=CARTESIAN_POINT ( 'NONE',  ( -0.5560430376289927645, 4.887756486939889733, -49.01410749632500341 ) ) ;
#2443=CARTESIAN_POINT ( 'NONE',  ( 2.062924749200377939, -4.402521781607152462, -68.10000000002503384 ) ) ;
#2450=CARTESIAN_POINT ( 'NONE',  ( -1.449312944839809658, 3.998683954144026220, -69.55099036452500627 ) ) ;
#2455=CARTESIAN_POINT ( 'NONE',  ( 4.315256771988532414, 1.538274589489400990, -45.92627377572499370 ) ) ;
#2486=CARTESIAN_POINT ( 'NONE',  ( 0.8945918243927832858, -4.819150861182647461, -58.74125695792500323 ) ) ;
#2521=CARTESIAN_POINT ( 'NONE',  ( -1.460566089872937789, -4.291843709425559261, -47.39520033292500045 ) ) ;
#2589=CARTESIAN_POINT ( 'NONE',  ( 1.746469154276752089, -4.581628552928044051, -68.10000000002500542 ) ) ;
#2597=CARTESIAN_POINT ( 'NONE',  ( -5.434147616959247529, -3.211087428728324866, -68.80382590962500444 ) ) ;
#2601=CARTESIAN_POINT ( 'NONE',  ( -4.568101251964836074, -0.2431723019727868862, -65.56421022022500722 ) ) ;
#2627=CARTESIAN_POINT ( 'NONE',  ( 0.000000000000000000, 0.000000000000000000, 0.000000000000000000 ) ) ;
#2632=CARTESIAN_POINT ( 'NONE',  ( -4.907595108193963718, 2.436408417516491287, -57.59877225282500746 ) ) ;
#2654=CARTESIAN_POINT ( 'NONE',  ( 4.248246898893026646, -2.821772188863608921, -43.35875473022499449 ) ) ;
#2668=CARTESIAN_POINT ( 'NONE',  ( 1.634888019277636051, 4.633891277622259608, -45.49079303332499791 ) ) ;
#2698=CARTESIAN_POINT ( 'NONE',  ( -2.744116393020877620, -4.299119443564640264, -68.10000000002500542 ) ) ;
#2742=CARTESIAN_POINT ( 'NONE',  ( 3.599561039394925999, 4.779710538172339263, -54.14619010302499191 ) ) ;
#2754=( GEOMETRIC_REPRESENTATION_CONTEXT ( 3 ) GLOBAL_UNCERTAINTY_ASSIGNED_CONTEXT ( ( #28883 ) ) GLOBAL_UNIT_ASSIGNED_CONTEXT ( ( #14838, #10569, #19707 ) ) REPRESENTATION_CONTEXT ( 'NONE', 'WORKASPACE' ) );
#2755=CARTESIAN_POINT ( 'NONE',  ( -5.606848515966891711, 1.848691355091094835, -68.74019511502498858 ) ) ;
#2761=CARTESIAN_POINT ( 'NONE',  ( 3.357378826396556271, -2.722208303779470651, -55.40923804942499942 ) ) ;
#2789=CARTESIAN_POINT ( 'NONE',  ( -3.174852331340443534, -3.764700477890503549, -59.92407541852500685 ) ) ;
#2794=EDGE_CURVE ( 'NONE', #5941, #1473, #21370, .T. ) ;
#2805=CARTESIAN_POINT ( 'NONE',  ( 2.868523387327241991, -3.581275371925169537, -44.10000000002499121 ) ) ;
#2812=CARTESIAN_POINT ( 'NONE',  ( 1.970249664213433727, 5.584433078155761621, -44.69079303332500075 ) ) ;
#2823=CARTESIAN_POINT ( 'NONE',  ( 2.534862810676351330, -4.171999357468124003, -46.56669147672499065 ) ) ;
#2826=SHAPE_DEFINITION_REPRESENTATION ( #18689, #19806 ) ;
#2861=CARTESIAN_POINT ( 'NONE',  ( -4.797151926237309461, -1.386351552423990219, -44.10000000002498410 ) ) ;
#2890=CARTESIAN_POINT ( 'NONE',  ( 2.752605500610148859, 3.655072764496607007, -54.62619010302499589 ) ) ;
#2895=CARTESIAN_POINT ( 'NONE',  ( -4.533384324195958825, 1.003679825387874924, -68.10000000002499121 ) ) ;
#2909=CARTESIAN_POINT ( 'NONE',  ( 1.634888019277636051, 4.633891277622259608, -45.49079303332499791 ) ) ;
#2939=CARTESIAN_POINT ( 'NONE',  ( 5.242919931573567283, -2.735361231296036699, -61.79790713612500497 ) ) ;
#2955=CARTESIAN_POINT ( 'NONE',  ( 2.594524747302418444, -3.974221016099061199, -44.10000000002499121 ) ) ;
#2964=CARTESIAN_POINT ( 'NONE',  ( -6.340437944841875506, 0.6332316896323284539, -47.62737393802499497 ) ) ;
#2979=CARTESIAN_POINT ( 'NONE',  ( 4.085013927406620837, 4.246146200131522441, -49.49426496242500662 ) ) ;
#3014=CARTESIAN_POINT ( 'NONE',  ( -4.685889913869174528, 0.7077737262620402703, -44.10000000002499121 ) ) ;
#3041=CARTESIAN_POINT ( 'NONE',  ( 0.7192951553310067414, 4.518739695591652783, -54.01500058692499806 ) ) ;
#3046=CARTESIAN_POINT ( 'NONE',  ( -4.256836137300013867, 0.9512594216477614495, -68.10000000002500542 ) ) ;
#3086=CARTESIAN_POINT ( 'NONE',  ( 1.387947292976102087, 4.364053279572885025, -60.46492395752500215 ) ) ;
#3102=CARTESIAN_POINT ( 'NONE',  ( 2.824297055372420040, -3.680463102343676240, -44.10000000002499121 ) ) ;
#3111=CARTESIAN_POINT ( 'NONE',  ( 1.634888019277636051, 4.633891277622259608, -45.49079303332499791 ) ) ;
#3123=CARTESIAN_POINT ( 'NONE',  ( -0.8137756071791968360, 4.795696781221863603, -52.00792092402499378 ) ) ;
#3193=CARTESIAN_POINT ( 'NONE',  ( 4.569612387855602087, -0.08076758077263958280, -57.69793411332500455 ) ) ;
#3197=CARTESIAN_POINT ( 'NONE',  ( -4.293412589747293673, 1.066240861064407408, -68.10000000002500542 ) ) ;
#3209=CARTESIAN_POINT ( 'NONE',  ( -4.892971904093138313, 0.02481116134537240947, -61.82122063472499462 ) ) ;
#3234=CARTESIAN_POINT ( 'NONE',  ( -2.098441946322436635, -3.287561928151557122, -68.10000000002500542 ) ) ;
#3241=CARTESIAN_POINT ( 'NONE',  ( -0.9941633020186212422, 5.428540911361258381, -61.05324387862498980 ) ) ;
#3258=CARTESIAN_POINT ( 'NONE',  ( 1.806849487525330922, -4.550967181663256866, -44.10000000002499121 ) ) ;
#3265=CARTESIAN_POINT ( 'NONE',  ( -2.571638601809290936, 3.775240214263654526, -48.05391720702499470 ) ) ;
#3278=CARTESIAN_POINT ( 'NONE',  ( 0.7122403016127445419, -5.223333760075516530, -50.51468436622500491 ) ) ;
#3343=CARTESIAN_POINT ( 'NONE',  ( 1.169850847344618083, -6.301966510834352775, -58.26125695792499926 ) ) ;
#3348=CARTESIAN_POINT ( 'NONE',  ( -4.626447879532794794, 0.8429120229185599333, -68.10000000002501963 ) ) ;
#3357=CARTESIAN_POINT ( 'NONE',  ( 0.8372177269581546621, 4.490875019823945991, -63.42744533512499316 ) ) ;
#3391=CARTESIAN_POINT ( 'NONE',  ( -1.078772944755383767, 5.890544393200768170, -60.25324387862499975 ) ) ;
#3409=CARTESIAN_POINT ( 'NONE',  ( 2.609296296073386756, -3.958891508797615977, -44.10000000002499831 ) ) ;
#3417=CARTESIAN_POINT ( 'NONE',  ( -0.5163256777700186984, 4.538631023554798638, -48.26410749632499630 ) ) ;
#3430=CARTESIAN_POINT ( 'NONE',  ( -5.206543681532186163, -1.819677770405741413, -51.20743646232500623 ) ) ;
#3457=VERTEX_POINT ( 'NONE', #14497 ) ;
#3500=CARTESIAN_POINT ( 'NONE',  ( -5.325262776967106149, 2.643762325382013945, -56.31877225282499211 ) ) ;
#3505=CARTESIAN_POINT ( 'NONE',  ( -4.251069959271740473, 0.9221155341078968171, -68.10000000002500542 ) ) ;
#3513=CARTESIAN_POINT ( 'NONE',  ( -5.941465883516308999, 0.03012783874251079297, -62.57122063482501062 ) ) ;
#3535=CARTESIAN_POINT ( 'NONE',  ( 6.136659917679837761, 0.6935318534637759935, -55.01771407622499765 ) ) ;
#3544=CARTESIAN_POINT ( 'NONE',  ( 0.6518654482653677418, -3.960075354149236393, -68.10000000002500542 ) ) ;
#3548=CARTESIAN_POINT ( 'NONE',  ( -2.098441946322436635, -3.287561928151557122, -68.10000000002500542 ) ) ;
#3551=CARTESIAN_POINT ( 'NONE',  ( -5.475468559288758641, 0.02776487098956707464, -63.37122063482500067 ) ) ;
#3574=CARTESIAN_POINT ( 'NONE',  ( 4.432674687120906398, 4.607520344841867121, -48.21426496242499837 ) ) ;
#3584=CARTESIAN_POINT ( 'NONE',  ( 4.669144396295984656, -2.892150817486062397, -50.13324460762500223 ) ) ;
#3652=CARTESIAN_POINT ( 'NONE',  ( -3.855177830964256813, -4.571422008809257420, -58.69407541852499577 ) ) ;
#3669=CARTESIAN_POINT ( 'NONE',  ( -5.475468559288758641, 0.02776487098956707464, -61.77122063472499036 ) ) ;
#3692=CARTESIAN_POINT ( 'NONE',  ( -0.9881560945370695404, 5.823346091562972227, -51.25792092402499378 ) ) ;
#3699=CARTESIAN_POINT ( 'NONE',  ( 2.723675539006792157, -3.828301447610997332, -68.10000000002499121 ) ) ;
#3703=CARTESIAN_POINT ( 'NONE',  ( -4.216405105086598049, 0.6620460458895751632, -44.10000000002499121 ) ) ;
#3708=CARTESIAN_POINT ( 'NONE',  ( -1.219854050253890598, 4.750520449216602437, -66.20876360982499875 ) ) ;
#3735=CARTESIAN_POINT ( 'NONE',  ( 4.172426907288941500, -2.584475198598515266, -48.58324460762500507 ) ) ;
#3755=CARTESIAN_POINT ( 'NONE',  ( -4.320323480314920417, -1.509945384023513082, -50.40743646232499486 ) ) ;
#3824=CARTESIAN_POINT ( 'NONE',  ( 5.975646968830259809, -0.1056191442178888718, -57.61793411332499915 ) ) ;
#3830=CARTESIAN_POINT ( 'NONE',  ( -3.194602321395983768, -2.288596850062932564, -68.10000000002500542 ) ) ;
#3839=CARTESIAN_POINT ( 'NONE',  ( 2.994727039187461415, -3.426347720743794234, -64.49605006312501132 ) ) ;
#3863=CARTESIAN_POINT ( 'NONE',  ( 2.384187449509611589, -3.542147544710181339, -68.10000000002500542 ) ) ;
#3867=CARTESIAN_POINT ( 'NONE',  ( -4.054871305269121429, -0.4479528304393000093, -44.10000000002499121 ) ) ;
#3872=CARTESIAN_POINT ( 'NONE',  ( 3.916181512753878824, -4.480608557854155904, -64.49605006312501132 ) ) ;
#3897=CARTESIAN_POINT ( 'NONE',  ( 3.874396413951474827, -2.399869827310081583, -48.93324460762499939 ) ) ;
#3907=CARTESIAN_POINT ( 'NONE',  ( -4.535753307212162078, -3.367775055652930227, -56.27895058492499913 ) ) ;
#3947=CARTESIAN_POINT ( 'NONE',  ( 3.248659393266399409, -2.157825791482659294, -43.35875473022499449 ) ) ;
#3978=CARTESIAN_POINT ( 'NONE',  ( 2.840551633548176191, -3.955783487875848881, -60.77197827312500067 ) ) ;
#3995=CARTESIAN_POINT ( 'NONE',  ( 3.542472921321142110, 4.818407451951889797, -66.64226422552501106 ) ) ;
#4014=CARTESIAN_POINT ( 'NONE',  ( -5.473571180597741836, 3.247285761689575168, -50.83267869292499341 ) ) ;
#4023=CARTESIAN_POINT ( 'NONE',  ( 2.875741676304124361, -3.508796633370238283, -68.10000000002500542 ) ) ;
#4028=CARTESIAN_POINT ( 'NONE',  ( 2.708949881112989289, 3.684664522020659305, -67.04226422542501496 ) ) ;
#4055=CARTESIAN_POINT ( 'NONE',  ( 0.6613659943794023555, -4.850238491497668392, -49.76468436622499780 ) ) ;
#4066=CARTESIAN_POINT ( 'NONE',  ( -3.469775141979342337, 3.953596984337869547, -54.73587006832500634 ) ) ;
#4094=MECHANICAL_DESIGN_GEOMETRIC_PRESENTATION_REPRESENTATION('',(#2084),#8744);
#4131=CARTESIAN_POINT ( 'NONE',  ( -4.880917369133354278, -2.481566535878938495, -61.56424626872499317 ) ) ;
#4139=CARTESIAN_POINT ( 'NONE',  ( -3.579340629180964850, -1.721930992784151293, -68.10000000002500542 ) ) ;
#4152=CARTESIAN_POINT ( 'NONE',  ( 1.257215589593053906, -4.341675124665346885, -67.70367649352500905 ) ) ;
#4171=CARTESIAN_POINT ( 'NONE',  ( -3.855177830964256813, -4.571422008809257420, -59.17407541852499975 ) ) ;
#4177=CARTESIAN_POINT ( 'NONE',  ( 1.806982085357143886, -3.734583774770322329, -68.10000000002501963 ) ) ;
#4183=CARTESIAN_POINT ( 'NONE',  ( 3.051761028451055680, 3.858721280585067248, -64.38768011632501498 ) ) ;
#4207=CARTESIAN_POINT ( 'NONE',  ( 0.7122403016127445419, -5.223333760075516530, -49.01468436622501201 ) ) ;
#4218=CARTESIAN_POINT ( 'NONE',  ( 3.599561039400463347, 4.779710538180673041, -55.10619010302499987 ) ) ;
#4260=CARTESIAN_POINT ( 'NONE',  ( -6.005838698572866008, -2.164963525412170853, -44.89497819512499177 ) ) ;
#4268=ORIENTED_EDGE ( 'NONE', *, *, #2794, .F. ) ;
#4294=CARTESIAN_POINT ( 'NONE',  ( 2.637655088286918748, -3.673227524439518277, -61.12197827312499498 ) ) ;
#4312=CARTESIAN_POINT ( 'NONE',  ( 1.257215589593047023, -4.341675124665348662, -67.30367649362501936 ) ) ;
#4338=CARTESIAN_POINT ( 'NONE',  ( 2.811346118373302172, -3.703141056614425164, -68.10000000002500542 ) ) ;
#4343=CARTESIAN_POINT ( 'NONE',  ( 4.782773383985687410, -2.143867810226098847, -68.02841551502500295 ) ) ;
#4365=CARTESIAN_POINT ( 'NONE',  ( 4.046071919037112607, -3.280610007121229188, -54.60923804942499515 ) ) ;
#4373=CARTESIAN_POINT ( 'NONE',  ( 2.097865490181829884, -3.779070126327673140, -55.58172062782499268 ) ) ;
#4414=CARTESIAN_POINT ( 'NONE',  ( -1.677440080217387219, -4.586793301645948340, -44.73640794712499513 ) ) ;
#4447=CARTESIAN_POINT ( 'NONE',  ( 1.494712469390715892, 4.699749685697345747, -59.71492395752500926 ) ) ;
#4466=CARTESIAN_POINT ( 'NONE',  ( -0.8291470764733299692, -4.443337602648613327, -67.90745670422499813 ) ) ;
#4483=CARTESIAN_POINT ( 'NONE',  ( 3.705709820302785396, 4.685590126413917034, -63.63768011632500787 ) ) ;
#4490=CARTESIAN_POINT ( 'NONE',  ( 0.8796424051323141757, -4.905285046648036662, -68.10000000002500542 ) ) ;
#4499=CARTESIAN_POINT ( 'NONE',  ( 4.441146713721671802, -1.990734395214990071, -67.27841551502500295 ) ) ;
#4523=CARTESIAN_POINT ( 'NONE',  ( 2.097865490181839654, -3.779070126327678025, -55.18172062782500120 ) ) ;
#4530=CARTESIAN_POINT ( 'NONE',  ( -3.985743628842677300, -2.180176701716181942, -53.74982952342499232 ) ) ;
#4566=CARTESIAN_POINT ( 'NONE',  ( 0.7190444496271986008, -5.886645524271489904, -44.26057807742500216 ) ) ;
#4609=CARTESIAN_POINT ( 'NONE',  ( -1.449312944839809658, 3.998683954144026220, -68.75099036452500911 ) ) ;
#4628=CARTESIAN_POINT ( 'NONE',  ( -5.973670867983248201, -0.3179945487330332332, -65.56421022022500722 ) ) ;
#4637=CARTESIAN_POINT ( 'NONE',  ( -0.9048066599225317308, -5.015669600398491745, -68.10000000002501963 ) ) ;
#4638=CARTESIAN_POINT ( 'NONE',  ( -4.849877185155405890, 0.08414189257355281226, -68.10000000002500542 ) ) ;
#4641=CARTESIAN_POINT ( 'NONE',  ( -4.882699615093633483, -0.1730453822568271960, -44.10000000002499121 ) ) ;
#4648=CARTESIAN_POINT ( 'NONE',  ( 4.569612387855602087, -0.08076758077263379576, -58.09793411332499602 ) ) ;
#4652=PRODUCT_DEFINITION ( 'UNKNOWN', '', #21403, #10614 ) ;
#4683=CARTESIAN_POINT ( 'NONE',  ( -4.566814987872939824, -1.843056667269423743, -60.13491726642500623 ) ) ;
#4707=CARTESIAN_POINT ( 'NONE',  ( 0.5498575204270228500, -4.501552459765379766, -43.38057807742500671 ) ) ;
#4724=CARTESIAN_POINT ( 'NONE',  ( 5.643028086411650435, 2.011589847869324377, -46.40627377572500478 ) ) ;
#4814=CARTESIAN_POINT ( 'NONE',  ( -1.895255389310859684, 5.229048247678121264, -69.63099036452499035 ) ) ;
#4818=CARTESIAN_POINT ( 'NONE',  ( -4.848570193085766533, 0.4842359979205582143, -47.62737393802499497 ) ) ;
#4845=CARTESIAN_POINT ( 'NONE',  ( 1.169850847344618083, -6.301966510834352775, -58.74125695792500323 ) ) ;
#4868=CARTESIAN_POINT ( 'NONE',  ( -1.557622931652903331, -4.259165208650873780, -43.58640794712500366 ) ) ;
#4878=CARTESIAN_POINT ( 'NONE',  ( 3.389692407805919849, 3.523397910813145906, -49.09426496242500093 ) ) ;
#4941=CARTESIAN_POINT ( 'NONE',  ( 1.415268835064556363, -5.780081730213937341, -64.70397119102500483 ) ) ;
#4946=CARTESIAN_POINT ( 'NONE',  ( 0.2112796128213221825, -5.021789149852340373, -68.10000000002501963 ) ) ;
#4948=CARTESIAN_POINT ( 'NONE',  ( -4.886044239781965004, -0.7344065197421389968, -68.10000000002503384 ) ) ;
#4955=CARTESIAN_POINT ( 'NONE',  ( 0.2444022557069394641, 3.892334458579130185, -69.35875473022500159 ) ) ;
#4960=CARTESIAN_POINT ( 'NONE',  ( 2.752605500610148859, 3.655072764496607007, -54.62619010302499589 ) ) ;
#4992=CARTESIAN_POINT ( 'NONE',  ( -3.468517234904579194, -2.575357395510371461, -56.27895058492499913 ) ) ;
#5008=CARTESIAN_POINT ( 'NONE',  ( -2.501313136143258120, -4.446574868790201585, -44.10000000002499121 ) ) ;
#5029=CARTESIAN_POINT ( 'NONE',  ( 1.634888019277630278, 4.633891277622259608, -45.89079303332500359 ) ) ;
#5067=B_SPLINE_CURVE_WITH_KNOTS ( 'NONE', 3,
 ( #28710, #5097, #21948, #28563, #29165, #24003, #28861, #9985, #24149, #21641, #9353, #9668, #89, #7612, #7315, #7005, #4948, #246, #14560, #2131, #9828, #19424, #16592, #4638, #29015, #11722, #30927, #18956, #19739, #20191, #17364, #15017, #15159, #26970, #22566, #557, #8214, #3348, #12488, #14868, #24762, #1009, #855, #24460, #2895, #5711, #25073, #10298, #5406, #17661, #10138, #29639, #29318, #22100, #27426, #24612, #3197, #10446, #22410, #7766, #19895, #3046, #3505, #5863, #5259, #12955, #20041, #29478, #20347, #17818, #15471, #7913, #15320, #5557, #13101, #8067, #10598, #17519, #27274, #12637, #24921, #29784, #22711, #22249, #1154, #10746, #12804, #29943, #705, #17208, #27124, #26812, #8532, #27581, #20503, #27900, #25865, #11381, #1631, #6024, #4139, #11221, #6342, #3830, #8849, #20822, #30431 ),
 .UNSPECIFIED., .F., .F.,
 ( 4, 2, 2, 2, 2, 2, 2, 1, 2, 2, 1, 1, 2, 2, 1, 1, 2, 2, 1, 1, 1, 2, 2, 1, 1, 1, 2, 2, 1, 1, 1, 2, 2, 1, 1, 1, 1, 2, 2, 1, 1, 1, 2, 2, 1, 1, 1, 1, 2, 2, 1, 1, 1, 2, 2, 1, 1, 1, 2, 2, 1, 1, 2, 2, 1, 2, 2, 1, 2, 2, 4 ),
 ( 0.000000000000000000, 0.06250000000000298372, 0.1250000000000060230, 0.1875000000000090761, 0.2500000000000121014, 0.2812500000000136557, 0.3125000000000152101, 0.3437500000000167644, 0.3593750000000174860, 0.3750000000000182632, 0.4062500000000197620, 0.4218750000000205391, 0.4296875000000209277, 0.4375000000000212608, 0.4531250000000220379, 0.4609375000000223155, 0.4648437500000224820, 0.4687500000000225930, 0.4843750000000232592, 0.4921875000000235367, 0.4960937500000237033, 0.4980468750000237588, 0.5000000000000238698, 0.5078125000000240918, 0.5117187500000242029, 0.5136718750000242029, 0.5146484375000240918, 0.5156250000000240918, 0.5234375000000235367, 0.5273437500000233147, 0.5292968750000232037, 0.5302734375000230926, 0.5312500000000229816, 0.5390625000000220934, 0.5429687500000215383, 0.5449218750000213163, 0.5458984375000212053, 0.5463867187500212053, 0.5468750000000212053, 0.5546875000000200950, 0.5585937500000194289, 0.5605468750000190958, 0.5615234375000189848, 0.5625000000000189848, 0.5703125000000183187, 0.5742187500000180966, 0.5761718750000179856, 0.5771484375000178746, 0.5776367187500177636, 0.5781250000000177636, 0.5859375000000174305, 0.5898437500000173195, 0.5917968750000170974, 0.5927734375000170974, 0.5937500000000169864, 0.6093750000000160982, 0.6171875000000156541, 0.6210937500000154321, 0.6230468750000153211, 0.6250000000000152101, 0.6562500000000137668, 0.6718750000000131006, 0.6796875000000127676, 0.6875000000000125455, 0.7187500000000112133, 0.7343750000000106581, 0.7500000000000099920, 0.8125000000000075495, 0.8437500000000063283, 0.8750000000000049960, 1.000000000000000000 ),
 .UNSPECIFIED. ) ;
#5094=CARTESIAN_POINT ( 'NONE',  ( -5.212126283948660621, -2.851000302232811201, -53.34982952342500084 ) ) ;
#5097=CARTESIAN_POINT ( 'NONE',  ( -2.954164893002536374, -4.165023816410697854, -68.10000000002500542 ) ) ;
#5106=CARTESIAN_POINT ( 'NONE',  ( -5.007939960741254026, -2.959237434304809788, -69.12382590962499762 ) ) ;
#5111=CARTESIAN_POINT ( 'NONE',  ( -0.5163256777700186984, 4.538631023554798638, -48.26410749632499630 ) ) ;
#5137=CARTESIAN_POINT ( 'NONE',  ( -3.552810942249358117, -4.212879106168850640, -59.97407541852498980 ) ) ;
#5152=CARTESIAN_POINT ( 'NONE',  ( 2.416185723194861357, -3.531454376423425856, -44.10000000002499121 ) ) ;
#5173=CARTESIAN_POINT ( 'NONE',  ( -3.362912017748242999, 4.936852587875802278, -48.05391720692499291 ) ) ;
#5253=CARTESIAN_POINT ( 'NONE',  ( -5.939015604524707115, -0.1501891088408410790, -53.07673954922500315 ) ) ;
#5259=CARTESIAN_POINT ( 'NONE',  ( -4.247090937810456879, 0.9000947937473684490, -68.10000000002501963 ) ) ;
#5269=CARTESIAN_POINT ( 'NONE',  ( 0.6613659943794023555, -4.850238491497668392, -49.76468436622499780 ) ) ;
#5303=CARTESIAN_POINT ( 'NONE',  ( 4.921121033118705412, -0.08698047164986451307, -58.84793411332501023 ) ) ;
#5318=CARTESIAN_POINT ( 'NONE',  ( 2.662870350918720597, -3.902358757652288901, -44.10000000002498410 ) ) ;
#5325=CARTESIAN_POINT ( 'NONE',  ( -6.340437944841875506, 0.6332316896323284539, -47.14737393802499810 ) ) ;
#5336=CARTESIAN_POINT ( 'NONE',  ( -2.769456955792640951, 4.065643307668772799, -48.80391720702499470 ) ) ;
#5402=CARTESIAN_POINT ( 'NONE',  ( 0.7192951553254764985, 4.518739695583327887, -54.41500058692499664 ) ) ;
#5406=CARTESIAN_POINT ( 'NONE',  ( -4.444041428977288710, 1.101146991380681728, -68.10000000002500542 ) ) ;
#5452=CARTESIAN_POINT ( 'NONE',  ( -3.351703491987489958, 4.047634511443764183, -63.74933298492499034 ) ) ;
#5465=CARTESIAN_POINT ( 'NONE',  ( 2.770284657207440659, -3.443617497140548434, -44.10000000002499831 ) ) ;
#5473=CARTESIAN_POINT ( 'NONE',  ( -1.572917327626556228, -4.621985533170462901, -46.24520033292499477 ) ) ;
#5487=CARTESIAN_POINT ( 'NONE',  ( -0.9881560945370695404, 5.823346091562972227, -51.25792092402499378 ) ) ;
#5528=SURFACE_STYLE_USAGE ( .BOTH. , #15284 ) ;
#5553=CARTESIAN_POINT ( 'NONE',  ( -4.499599993570057244, -1.182519567789861004, -55.70102360502500005 ) ) ;
#5557=CARTESIAN_POINT ( 'NONE',  ( -4.222392096712967557, 0.7175927990900473619, -68.10000000002500542 ) ) ;
#5568=CARTESIAN_POINT ( 'NONE',  ( -4.069925668896384963, 4.914984763948436530, -62.99933298482500277 ) ) ;
#5602=CARTESIAN_POINT ( 'NONE',  ( 1.815007998551255941, 5.706838904126064094, -60.94492395752499903 ) ) ;
#5619=CARTESIAN_POINT ( 'NONE',  ( 2.852595256171609250, -3.624945453263371586, -44.10000000002499831 ) ) ;
#5627=CARTESIAN_POINT ( 'NONE',  ( 4.880217822150678231, -0.7240669684095875080, -45.38818262062500253 ) ) ;
#5641=CARTESIAN_POINT ( 'NONE',  ( 5.363076718300177959, -2.525690298526013677, -52.29872167392500160 ) ) ;
#5706=CARTESIAN_POINT ( 'NONE',  ( -4.535753307212162078, -3.367775055652930227, -55.79895058492499516 ) ) ;
#5711=CARTESIAN_POINT ( 'NONE',  ( -4.502786141747646909, 1.045045138632145321, -68.10000000002500542 ) ) ;
#5723=CARTESIAN_POINT ( 'NONE',  ( 0.9016190905398319133, 4.836326944446648568, -62.67744533512500738 ) ) ;
#5758=CARTESIAN_POINT ( 'NONE',  ( 1.815007998551255941, 5.706838904126064094, -60.46492395752500215 ) ) ;
#5774=CARTESIAN_POINT ( 'NONE',  ( 2.725151615585481135, -3.829855452310775288, -44.10000000002499121 ) ) ;
#5781=( NAMED_UNIT ( * ) SI_UNIT ( $, .STERADIAN. ) SOLID_ANGLE_UNIT ( ) );
#5784=CARTESIAN_POINT ( 'NONE',  ( -3.948109860491266776, 2.321589337205137937, -44.44354844312501029 ) ) ;
#5798=CARTESIAN_POINT ( 'NONE',  ( -5.649653782182448403, -1.974543963569185046, -50.40743646232499486 ) ) ;
#5858=CARTESIAN_POINT ( 'NONE',  ( -5.463799992266447525, -1.435916617982112342, -56.45102360502500005 ) ) ;
#5863=CARTESIAN_POINT ( 'NONE',  ( -4.248672686832829726, 0.9089880553856074519, -68.10000000002501963 ) ) ;
#5872=CARTESIAN_POINT ( 'NONE',  ( -5.973670867983248201, -0.3179945487330332332, -65.56421022022500722 ) ) ;
#5891=CARTESIAN_POINT ( 'NONE',  ( -6.340437944841875506, 0.6332316896323284539, -47.62737393802499497 ) ) ;
#5902=CARTESIAN_POINT ( 'NONE',  ( -1.903575822388091643, -3.411965078385457595, -68.10000000002500542 ) ) ;
#5907=CARTESIAN_POINT ( 'NONE',  ( -1.494970809075166329, -6.161113191638062148, -61.94311227092499195 ) ) ;
#5931=( NAMED_UNIT ( * ) PLANE_ANGLE_UNIT ( ) SI_UNIT ( $, .RADIAN. ) );
#5933=CARTESIAN_POINT ( 'NONE',  ( 0.7970308137830555140, -5.845159207773487076, -48.96468436622500775 ) ) ;
#5941=VERTEX_POINT ( 'NONE', #21470 ) ;
#5947=CARTESIAN_POINT ( 'NONE',  ( 4.545032752014868116, -0.3361547907463890428, -49.52442242802500516 ) ) ;
#6018=CARTESIAN_POINT ( 'NONE',  ( -3.174852331340443534, -3.764700477890503549, -58.42407541852500685 ) ) ;
#6024=CARTESIAN_POINT ( 'NONE',  ( -3.732454924695358223, -1.410253583585163284, -68.10000000002500542 ) ) ;
#6032=CARTESIAN_POINT ( 'NONE',  ( -1.219854050253892153, 4.750520449216608654, -65.80876360982500728 ) ) ;
#6053=CARTESIAN_POINT ( 'NONE',  ( 1.728540313474559387, 5.648005006634932990, -51.46125421262499344 ) ) ;
#6062=CARTESIAN_POINT ( 'NONE',  ( 2.530566566541730289, -4.038018835116537808, -68.10000000002500542 ) ) ;
#6064=CARTESIAN_POINT ( 'NONE',  ( -3.736258300216923178, -1.388188646204749910, -44.10000000002499121 ) ) ;
#6067=CARTESIAN_POINT ( 'NONE',  ( -5.296314592117303377, -2.692763687817543161, -62.84424626872499431 ) ) ;
#6089=CARTESIAN_POINT ( 'NONE',  ( 4.545032752014868116, -0.3361547907463890428, -48.72442242802500090 ) ) ;
#6100=CARTESIAN_POINT ( 'NONE',  ( 0.7970308137830555140, -5.845159207773487076, -50.56468436622500917 ) ) ;
#6173=CARTESIAN_POINT ( 'NONE',  ( -1.989652436383612555, 4.808159600214577445, -56.34652090042499850 ) ) ;
#6192=CARTESIAN_POINT ( 'NONE',  ( -2.911316102860724175, -3.927725552502973727, -65.13409070562501313 ) ) ;
#6210=CARTESIAN_POINT ( 'NONE',  ( 5.782578939028539367, 2.564649547393091478, -51.87998794302499306 ) ) ;
#6219=CARTESIAN_POINT ( 'NONE',  ( 2.876589613553454772, -3.520147964197292811, -68.10000000002500542 ) ) ;
#6225=CARTESIAN_POINT ( 'NONE',  ( -5.505147662666007413, -0.2930537997861774602, -66.36421022022500438 ) ) ;
#6256=CARTESIAN_POINT ( 'NONE',  ( 4.894650655971835462, -0.3620128515310818140, -48.37442242802500658 ) ) ;
#6268=CARTESIAN_POINT ( 'NONE',  ( -4.213298386693987041, 4.800796338109710071, -54.46587006832499611 ) ) ;
#6336=CARTESIAN_POINT ( 'NONE',  ( 4.317698767220935707, -2.252650425851481675, -60.56790713612500809 ) ) ;
#6342=CARTESIAN_POINT ( 'NONE',  ( -3.262900226955093519, -2.198300220329731935, -68.10000000002501963 ) ) ;
#6353=CARTESIAN_POINT ( 'NONE',  ( -5.434147616959247529, -3.211087428728324866, -67.84382590962499648 ) ) ;
#6372=CARTESIAN_POINT ( 'NONE',  ( -3.297371880451163584, -3.946021304934626883, -44.16141975532499941 ) ) ;
#6379=CARTESIAN_POINT ( 'NONE',  ( 2.613153378155294693, -3.469718638663583654, -68.10000000002500542 ) ) ;
#6383=CARTESIAN_POINT ( 'NONE',  ( -4.308414154086193548, 1.093458695205176801, -44.10000000002497700 ) ) ;
#6387=CARTESIAN_POINT ( 'NONE',  ( 1.304267357873228894, -5.326741986703369847, -65.50397119102498777 ) ) ;
#6391=CARTESIAN_POINT ( 'NONE',  ( -3.224145675551910895, -2.281186089468392186, -44.28462724592499455 ) ) ;
#6411=CARTESIAN_POINT ( 'NONE',  ( 5.943504367937093136, -0.4395870339238064362, -49.12442242802499948 ) ) ;
#6412=ADVANCED_FACE ( 'NONE', ( #6905 ), #24590, .T. ) ;
#6421=CARTESIAN_POINT ( 'NONE',  ( -1.293561172433232986, -6.216321778783836294, -52.92706695232499925 ) ) ;
#6487=CARTESIAN_POINT ( 'NONE',  ( -4.050122923326508584, -2.059172231882750559, -62.36424626872499033 ) ) ;
#6506=CARTESIAN_POINT ( 'NONE',  ( 3.264631907946181855, 4.440493141956372902, -65.84226422542499790 ) ) ;
#6534=CARTESIAN_POINT ( 'NONE',  ( 2.212761947522928985, -3.601507522846123077, -68.10000000002500542 ) ) ;
#6536=CARTESIAN_POINT ( 'NONE',  ( -3.961961208831939363, -0.8145944572358391200, -44.10000000002499121 ) ) ;
#6539=CARTESIAN_POINT ( 'NONE',  ( -5.001751348353093540, 2.318407806459778175, -66.57526299442500317 ) ) ;
#6562=CARTESIAN_POINT ( 'NONE',  ( 5.066518387468507356, -3.138291312573631586, -49.33324460762499797 ) ) ;
#6573=CARTESIAN_POINT ( 'NONE',  ( -1.192105394233154314, -5.728767129463715690, -53.72706695232499641 ) ) ;
#6610=CARTESIAN_POINT ( 'NONE',  ( 3.498556269673057884, -2.323812390827893815, -44.10875473022500159 ) ) ;
#6641=CARTESIAN_POINT ( 'NONE',  ( -5.623491485972666126, 3.092612689740418919, -59.81908057272499946 ) ) ;
#6655=ORIENTED_EDGE ( 'NONE', *, *, #30577, .T. ) ;
#6658=CARTESIAN_POINT ( 'NONE',  ( 5.384875807261761516, 2.601783486389667832, -66.85315453642499506 ) ) ;
#6684=CARTESIAN_POINT ( 'NONE',  ( 2.410831077383560839, -3.533047124804223671, -68.10000000002500542 ) ) ;
#6687=CARTESIAN_POINT ( 'NONE',  ( -3.771147929147382172, -1.309395846178109668, -44.10000000002499121 ) ) ;
#6693=CARTESIAN_POINT ( 'NONE',  ( 3.264631907946181855, 4.440493141956372902, -67.44226422552499400 ) ) ;
#6717=CARTESIAN_POINT ( 'NONE',  ( 3.615638736154061839, -2.931608942551765740, -54.65923804942499942 ) ) ;
#6726=CARTESIAN_POINT ( 'NONE',  ( 4.390418465364303025, -3.559810858781688125, -55.88923804942498919 ) ) ;
#6770=CARTESIAN_POINT ( 'NONE',  ( -3.948109860491266776, 2.321589337205137937, -44.84354844312500177 ) ) ;
#6802=CARTESIAN_POINT ( 'NONE',  ( -4.240613917342963113, -1.711409762446096439, -59.38491726642499202 ) ) ;
#6819=CARTESIAN_POINT ( 'NONE',  ( -4.185763533044374540, 4.163314928055855901, -68.46322600552500148 ) ) ;
#6835=CARTESIAN_POINT ( 'NONE',  ( -5.427432314178970429, 2.515719109140460041, -65.77526299442500601 ) ) ;
#6841=CARTESIAN_POINT ( 'NONE',  ( 1.909765729747931351, -4.496882425974528807, -68.10000000002501963 ) ) ;
#6844=CARTESIAN_POINT ( 'NONE',  ( -4.561137155964747336, 0.9634438910280386237, -44.10000000002499121 ) ) ;
#6848=CARTESIAN_POINT ( 'NONE',  ( -3.508509149563535434, -4.733412845334678209, -65.93409070562501029 ) ) ;
#6851=CARTESIAN_POINT ( 'NONE',  ( -2.901540723753613715, -2.679228086972462730, -44.22295181582499168 ) ) ;
#6869=CARTESIAN_POINT ( 'NONE',  ( 2.990129296507525680, -3.859048371143013245, -51.75430438132499944 ) ) ;
#6876=CARTESIAN_POINT ( 'NONE',  ( -3.221934060409654688, 3.671197199744478112, -54.38587006832499071 ) ) ;
#6896=CARTESIAN_POINT ( 'NONE',  ( -2.249420116617089072, -4.577155045439369019, -44.10000000002499121 ) ) ;
#6905=FACE_OUTER_BOUND ( 'NONE', #20955, .T. ) ;
#6921=CARTESIAN_POINT ( 'NONE',  ( -3.130203125555106158, 5.106303518385050033, -45.53531229042499717 ) ) ;
#6978=CARTESIAN_POINT ( 'NONE',  ( 0.2632024292269652954, 4.191744801550177257, -68.60875473022500159 ) ) ;
#6997=CARTESIAN_POINT ( 'NONE',  ( -5.296314592117303377, -2.692763687817543161, -62.36424626872499033 ) ) ;
#7004=CARTESIAN_POINT ( 'NONE',  ( 1.237533978107217214, -4.800969678198779178, -68.10000000002500542 ) ) ;
#7005=CARTESIAN_POINT ( 'NONE',  ( -4.876949263959866165, -0.8560970368912672601, -68.10000000002500542 ) ) ;
#7007=CARTESIAN_POINT ( 'NONE',  ( -4.887447097588012213, -0.7107402505946681659, -44.10000000002498410 ) ) ;
#7015=CARTESIAN_POINT ( 'NONE',  ( 2.534862810676351330, -4.171999357468124003, -46.56669147672499065 ) ) ;
#7035=CARTESIAN_POINT ( 'NONE',  ( 5.363076718300177959, -2.525690298526013677, -51.81872167392499762 ) ) ;
#7043=CARTESIAN_POINT ( 'NONE',  ( 4.003591150705129387, -2.204345408526039218, -58.30843849682500490 ) ) ;
#7066=CARTESIAN_POINT ( 'NONE',  ( -1.877135327876712667, -5.132840123261955156, -43.18640794712499797 ) ) ;
#7081=CARTESIAN_POINT ( 'NONE',  ( -6.340437944841875506, 0.6332316896323284539, -47.62737393802499497 ) ) ;
#7169=CARTESIAN_POINT ( 'NONE',  ( 4.531630834892032667, -0.6723478992683162847, -46.13818262062499542 ) ) ;
#7199=CARTESIAN_POINT ( 'NONE',  ( 5.235465350887244185, -2.882605534178610984, -58.30843849682499780 ) ) ;
#7238=CARTESIAN_POINT ( 'NONE',  ( -4.848570193085766533, 0.4842359979205582143, -47.62737393802499497 ) ) ;
#7314=CARTESIAN_POINT ( 'NONE',  ( 2.211450541897235222, -4.299781033209638892, -68.10000000002500542 ) ) ;
#7315=CARTESIAN_POINT ( 'NONE',  ( -4.859269776546366160, -1.038628159466365108, -68.10000000002500542 ) ) ;
#7327=CARTESIAN_POINT ( 'NONE',  ( -4.178199994060140199, -1.098053884355548737, -56.45102360502500005 ) ) ;
#7355=CARTESIAN_POINT ( 'NONE',  ( -5.623491485972666126, 3.092612689740418919, -60.29908057272499633 ) ) ;
#7377=CARTESIAN_POINT ( 'NONE',  ( 3.248659393266396300, -2.157825791482658850, -42.95875473022500302 ) ) ;
#7388=CARTESIAN_POINT ( 'NONE',  ( 2.534862810676351330, -4.171999357468123115, -46.96669147672501055 ) ) ;
#7461=AXIS2_PLACEMENT_3D ( 'NONE', #18551, #27992, #27673 ) ;
#7469=CARTESIAN_POINT ( 'NONE',  ( -1.746607907818665817, 4.818926816502865584, -69.95099036452499774 ) ) ;
#7476=CARTESIAN_POINT ( 'NONE',  ( -3.468517234904579194, -2.575357395510371461, -56.27895058492499913 ) ) ;
#7506=CARTESIAN_POINT ( 'NONE',  ( 5.235465350887244185, -2.882605534178610984, -58.78843849682499467 ) ) ;
#7531=CARTESIAN_POINT ( 'NONE',  ( 0.7190444496327288437, -5.886645524263159679, -43.30057807742499421 ) ) ;
#7543=CARTESIAN_POINT ( 'NONE',  ( -5.843148694310191793, 0.5835664591014033675, -48.42737393802499923 ) ) ;
#7609=CARTESIAN_POINT ( 'NONE',  ( -1.065285671501096765, -5.119323817795550902, -52.17706695232500635 ) ) ;
#7612=CARTESIAN_POINT ( 'NONE',  ( -4.829479218091812243, -1.221145322595682092, -68.10000000002503384 ) ) ;
#7624=CARTESIAN_POINT ( 'NONE',  ( -4.300317018729668206, 2.364939115720630980, -59.81908057272499946 ) ) ;
#7650=CARTESIAN_POINT ( 'NONE',  ( 4.311559700750661861, -2.373910439939187267, -59.05843849682499780 ) ) ;
#7665=CARTESIAN_POINT ( 'NONE',  ( 0.7487076883252210546, -3.952114498550206800, -44.10000000002500542 ) ) ;
#7673=CARTESIAN_POINT ( 'NONE',  ( -4.757978549728680839, 2.797812790916673897, -44.04354844312500461 ) ) ;
#7685=CARTESIAN_POINT ( 'NONE',  ( -1.909971040720825908, -5.612411004515823088, -47.47520033292499875 ) ) ;
#7728=CARTESIAN_POINT ( 'NONE',  ( -4.529613163810471299, 1.007793355091292531, -44.10000000002500542 ) ) ;
#7760=CARTESIAN_POINT ( 'NONE',  ( 3.346097069831758919, -4.318458891484066697, -51.70430438132500228 ) ) ;
#7766=CARTESIAN_POINT ( 'NONE',  ( -4.280718260511862994, 1.038266773289004075, -68.10000000002500542 ) ) ;
#7776=CARTESIAN_POINT ( 'NONE',  ( 4.406935161057896622, -1.569536819518615900, -67.23341453912500754 ) ) ;
#7806=CARTESIAN_POINT ( 'NONE',  ( -5.296314592117303377, -2.692763687817543161, -62.36424626872499033 ) ) ;
#7823=CARTESIAN_POINT ( 'NONE',  ( 2.130274636608692873, -3.629988127160616695, -44.10000000002499121 ) ) ;
#7829=CARTESIAN_POINT ( 'NONE',  ( -5.162912894389027230, 3.035924517800103750, -44.84354844312500177 ) ) ;
#7839=CARTESIAN_POINT ( 'NONE',  ( 4.942443250116775211, -2.327596941721505441, -53.09872167392499875 ) ) ;
#7877=CARTESIAN_POINT ( 'NONE',  ( -4.670117344778931034, 0.7466779630707167659, -44.10000000002499121 ) ) ;
#7909=CARTESIAN_POINT ( 'NONE',  ( -4.385510522250850585, 2.177216032694683445, -56.04877225282501030 ) ) ;
#7913=CARTESIAN_POINT ( 'NONE',  ( -4.223277344473779671, 0.7255220498998576906, -68.10000000002501963 ) ) ;
#7924=CARTESIAN_POINT ( 'NONE',  ( -5.973670867983248201, -0.3179945487330332332, -65.08421022022500324 ) ) ;
#7958=CARTESIAN_POINT ( 'NONE',  ( 0.9016190905398319133, 4.836326944446648568, -64.17744533512500027 ) ) ;
#7973=CARTESIAN_POINT ( 'NONE',  ( 2.219048841976018593, -3.599394683114398585, -44.10000000002499121 ) ) ;
#7979=FILL_AREA_STYLE_COLOUR ( '', #24199 ) ;
#7981=CARTESIAN_POINT ( 'NONE',  ( 2.137930486642451555, 6.059703978454344941, -45.49079303332499791 ) ) ;
#7995=CARTESIAN_POINT ( 'NONE',  ( 0.6613659943794023555, -4.850238491497668392, -49.76468436622499780 ) ) ;
#8061=CARTESIAN_POINT ( 'NONE',  ( -2.158984558600606007, 5.217364672555318883, -57.14652090042499566 ) ) ;
#8067=CARTESIAN_POINT ( 'NONE',  ( -4.217110537010221982, 0.6683951208602848526, -68.10000000002500542 ) ) ;
#8075=CARTESIAN_POINT ( 'NONE',  ( -4.919493655976348023, -0.2618778636732672083, -64.81421022022499301 ) ) ;
#8108=CARTESIAN_POINT ( 'NONE',  ( 0.8372177269581373427, 4.490875019823951320, -63.82744533512499885 ) ) ;
#8122=CARTESIAN_POINT ( 'NONE',  ( 1.927687739761373198, -3.697324211539649852, -44.10000000002500542 ) ) ;
#8127=SURFACE_SIDE_STYLE ('',( #10826 ) ) ;
#8129=CARTESIAN_POINT ( 'NONE',  ( -2.577814338686791107, 4.205191132749348526, -44.30531229042500740 ) ) ;
#8142=CARTESIAN_POINT ( 'NONE',  ( 4.172426907288941500, -2.584475198598515266, -50.08324460762499797 ) ) ;
#8209=CARTESIAN_POINT ( 'NONE',  ( 3.992508014903327407, 4.044424149039453908, -56.90805965152499368 ) ) ;
#8214=CARTESIAN_POINT ( 'NONE',  ( -4.643748704705192409, 0.8058717780413064968, -68.10000000002500542 ) ) ;
#8225=CARTESIAN_POINT ( 'NONE',  ( -3.135263495375002485, -4.229858287293371433, -64.38409070562499892 ) ) ;
#8264=CARTESIAN_POINT ( 'NONE',  ( 3.178712542294670040, -4.426710093576285310, -62.32197827312499783 ) ) ;
#8287=CARTESIAN_POINT ( 'NONE',  ( -5.221537131022022216, 0.5214849208526588509, -46.87737393802500918 ) ) ;
#8299=CARTESIAN_POINT ( 'NONE',  ( 5.329043336022200705, 2.363500563244980590, -52.67998794302499022 ) ) ;
#8365=CARTESIAN_POINT ( 'NONE',  ( -1.256295066205788347, -5.815478746186413694, -55.45033560642499992 ) ) ;
#8381=CARTESIAN_POINT ( 'NONE',  ( 3.916181512753878824, -4.480608557854155904, -64.49605006312501132 ) ) ;
#8398=CARTESIAN_POINT ( 'NONE',  ( -5.649653782182448403, -1.974543963569185046, -50.40743646232499486 ) ) ;
#8415=CARTESIAN_POINT ( 'NONE',  ( 4.009291712408942665, -2.091746824018185347, -61.71790713612498536 ) ) ;
#8431=CARTESIAN_POINT ( 'NONE',  ( -0.8531356284651092636, -3.830139717306812130, -44.10000000002499121 ) ) ;
#8440=CARTESIAN_POINT ( 'NONE',  ( -4.507646854653408752, 2.674235333181991692, -50.08267869292500052 ) ) ;
#8455=CARTESIAN_POINT ( 'NONE',  ( 0.8648632234848976363, -6.342619565911398638, -49.76468436622499780 ) ) ;
#8524=CARTESIAN_POINT ( 'NONE',  ( 4.003591150705128499, -2.204345408526048988, -57.90843849682499211 ) ) ;
#8532=CARTESIAN_POINT ( 'NONE',  ( -4.047171486430775289, -0.4744283861493229226, -68.10000000002499121 ) ) ;
#8543=CARTESIAN_POINT ( 'NONE',  ( -3.750715812471464350, 4.529495762826656780, -62.19933298482499850 ) ) ;
#8562=CARTESIAN_POINT ( 'NONE',  ( -5.712565024699335581, -0.3554524910389447734, -44.56408784452499816 ) ) ;
#8568=CARTESIAN_POINT ( 'NONE',  ( 2.819655859569989431, -3.689021998396972979, -68.10000000002499121 ) ) ;
#8573=DIRECTION ( 'NONE',  ( -0.5532886644841250590, -0.8329895880221872551, 0.000000000000000000 ) ) ;
#8575=CARTESIAN_POINT ( 'NONE',  ( 2.994727039187461415, -3.426347720743794234, -64.49605006312501132 ) ) ;
#8601=CARTESIAN_POINT ( 'NONE',  ( 4.669144396295984656, -2.892150817486062397, -48.53324460762500081 ) ) ;
#8611=CARTESIAN_POINT ( 'NONE',  ( -4.180007949804073419, -3.103635835586971758, -57.07895058492500340 ) ) ;
#8682=CARTESIAN_POINT ( 'NONE',  ( 5.896017893897736784, 2.415859114112482775, -60.41141554682499759 ) ) ;
#8699=CARTESIAN_POINT ( 'NONE',  ( 1.644051155559919764, -5.677575162961061572, -67.22367649362500686 ) ) ;
#8721=CARTESIAN_POINT ( 'NONE',  ( -1.256295066205788347, -5.815478746186413694, -55.93033560642499680 ) ) ;
#8731=CARTESIAN_POINT ( 'NONE',  ( 2.571935351011521487, -3.481578157327508194, -68.10000000002500542 ) ) ;
#8737=CARTESIAN_POINT ( 'NONE',  ( -4.469650141049659631, 2.071768678095493588, -66.52526299432499002 ) ) ;
#8744=( GEOMETRIC_REPRESENTATION_CONTEXT ( 3 ) GLOBAL_UNCERTAINTY_ASSIGNED_CONTEXT ( ( #21656 ) ) GLOBAL_UNIT_ASSIGNED_CONTEXT ( ( #620, #5931, #5781 ) ) REPRESENTATION_CONTEXT ( 'NONE', 'WORKASPACE' ) );
#8764=CARTESIAN_POINT ( 'NONE',  ( -0.9106536557280191513, 5.366613064759778950, -50.45792092402500373 ) ) ;
#8774=ORIENTED_EDGE ( 'NONE', *, *, #17309, .F. ) ;
#8775=CARTESIAN_POINT ( 'NONE',  ( 5.655353257545034040, 0.6391371982505194005, -55.81771407622498771 ) ) ;
#8840=CARTESIAN_POINT ( 'NONE',  ( -1.377718196578040954, -5.677888627607300620, -61.14311227092499479 ) ) ;
#8849=CARTESIAN_POINT ( 'NONE',  ( -2.827549391578647153, -2.736619477458235306, -68.10000000002501963 ) ) ;
#8860=CARTESIAN_POINT ( 'NONE',  ( -1.895255389310859684, 5.229048247678121264, -69.15099036452500059 ) ) ;
#8879=CARTESIAN_POINT ( 'NONE',  ( 5.975646968830259809, -0.1056191442178888718, -58.09793411332499602 ) ) ;
#8886=CARTESIAN_POINT ( 'NONE',  ( 2.446868394388314272, -3.520846267504715854, -68.10000000002500542 ) ) ;
#8891=CARTESIAN_POINT ( 'NONE',  ( -4.367877465460095365, 1.136530670978911362, -44.10000000002498410 ) ) ;
#8896=CARTESIAN_POINT ( 'NONE',  ( 2.994727039187459194, -3.426347720743798231, -64.89605006312500279 ) ) ;
#8923=CARTESIAN_POINT ( 'NONE',  ( 4.762123832160154890, 2.112064333128992555, -51.12998794302500016 ) ) ;
#8935=CARTESIAN_POINT ( 'NONE',  ( 6.136659917674307074, 0.6935318534554493208, -55.49771407622499453 ) ) ;
#9002=CARTESIAN_POINT ( 'NONE',  ( -5.623491485972666126, 3.092612689740418919, -59.33908057272499548 ) ) ;
#9020=CARTESIAN_POINT ( 'NONE',  ( -1.595193757947241497, 6.212219048941578059, -65.72876360962500542 ) ) ;
#9040=CARTESIAN_POINT ( 'NONE',  ( 0.9406167415608388538, 5.909121140422558760, -54.41500058692499664 ) ) ;
#9045=CARTESIAN_POINT ( 'NONE',  ( 2.841892371157072716, -3.648336829434535300, -68.10000000002500542 ) ) ;
#9050=CARTESIAN_POINT ( 'NONE',  ( -4.205204442357076466, 0.5518332366461318195, -44.10000000002499121 ) ) ;
#9054=CARTESIAN_POINT ( 'NONE',  ( -5.973670867977711296, -0.3179945487246996216, -66.04421022022501120 ) ) ;
#9078=CARTESIAN_POINT ( 'NONE',  ( 4.101176313917077820, -1.931410228222282921, -52.29872167392500160 ) ) ;
#9087=CARTESIAN_POINT ( 'NONE',  ( 3.615638736159595634, -2.931608942543439067, -56.15923804942499231 ) ) ;
#9152=CARTESIAN_POINT ( 'NONE',  ( -3.855177830964256813, -4.571422008809257420, -59.17407541852499975 ) ) ;
#9168=CARTESIAN_POINT ( 'NONE',  ( 5.384875807261761516, 2.601783486389667832, -66.37315453652500707 ) ) ;
#9188=CARTESIAN_POINT ( 'NONE',  ( 5.896017893897736784, 2.415859114112482775, -60.89141554682500157 ) ) ;
#9194=CARTESIAN_POINT ( 'NONE',  ( 2.667210884058451636, -3.897237072852844264, -68.10000000002501963 ) ) ;
#9202=CARTESIAN_POINT ( 'NONE',  ( -3.135263495386069632, -4.229858287310033660, -65.88409070562501313 ) ) ;
#9227=CARTESIAN_POINT ( 'NONE',  ( 0.7746255519315137228, 4.866335056773794854, -53.66500058692498953 ) ) ;
#9236=CARTESIAN_POINT ( 'NONE',  ( 2.743362564037614248, -4.941860934411918649, -56.06172062782499665 ) ) ;
#9265=CARTESIAN_POINT ( 'NONE',  ( -2.036891525988612894, -5.569677580567498509, -43.50640794712499826 ) ) ;
#9280=CARTESIAN_POINT ( 'NONE',  ( -2.036891525988612894, -5.569677580567498509, -44.46640794712500622 ) ) ;
#9330=CARTESIAN_POINT ( 'NONE',  ( -1.560798555979769464, 4.306275027539294697, -68.40099036452500059 ) ) ;
#9353=CARTESIAN_POINT ( 'NONE',  ( -4.679640823766034963, -1.817694234202872350, -68.10000000002500542 ) ) ;
#9355=CARTESIAN_POINT ( 'NONE',  ( -4.500610150543032262, 1.045894616594410076, -44.10000000002499831 ) ) ;
#9358=CARTESIAN_POINT ( 'NONE',  ( -4.155524648305278568, -2.455537445457764978, -68.72382590962500615 ) ) ;
#9362=CARTESIAN_POINT ( 'NONE',  ( -1.650988191866306742, 3.989749455477753504, -57.14652090042499566 ) ) ;
#9383=CARTESIAN_POINT ( 'NONE',  ( -3.221934060415182710, 3.671197199736151440, -53.58587006832498645 ) ) ;
#9393=ORIENTED_EDGE ( 'NONE', *, *, #15927, .T. ) ;
#9396=CARTESIAN_POINT ( 'NONE',  ( -0.06088579265679563285, 5.203211362304668519, -58.11818518972498993 ) ) ;
#9419=CARTESIAN_POINT ( 'NONE',  ( 0.6626488065419183782, -5.424947836070461271, -42.98057807742500103 ) ) ;
#9517=( BOUNDED_CURVE ( )  B_SPLINE_CURVE ( 5, ( #20378, #6372, #25260, #29969, #8562, #15498, #22904, #11408, #23063, #27608, #13610, #21010, #1659, #5891, #27766, #13294, #1344, #13763, #15649, #16124, #18162, #8398, #4014, #3692, #6053, #6210, #25102, #15819, #30614, #1507, #25426, #11251, #9040, #20860, #3535, #11099, #20693, #8721, #23385, #18329, #25735, #30458, #1186, #13131, #8879, #18482, #28081, #4171, #1819, #27450, #22740, #10782, #9188, #21472, #18636, #13927, #6997, #26194, #14085, #26045, #4483, #2286, #25894, #4941, #31069, #4628, #6835, #23535, #28399, #21631, #30918, #28847, #21780, #2122, #23687 ),
 .UNSPECIFIED., .F., .T. ) 
 B_SPLINE_CURVE_WITH_KNOTS ( ( 6, 3, 3, 3, 3, 3, 3, 3, 3, 3, 3, 3, 3, 3, 3, 3, 3, 3, 3, 3, 3, 3, 3, 3, 6 ),
 ( 8.127326494040000071, 11.49596029219999949, 23.35952330949999833, 35.23214498380000492, 46.71570041140000029, 58.48118637179999979, 70.16173614769999745, 81.99711437660000968, 93.33986353700001359, 104.8204913790000035, 116.3828353250000021, 128.2105526469999859, 137.7231253239999944, 147.2120576640000138, 156.6774103699999898, 168.4624398839999913, 180.2684855139999911, 192.1268167670000082, 203.5147100690000173, 215.0810220189999882, 226.8492753339999979, 238.4740513719999910, 250.2932425120000062, 262.1023078380000015, 271.0195818650000206 ),
 .UNSPECIFIED. ) 
 CURVE ( )  GEOMETRIC_REPRESENTATION_ITEM ( )  RATIONAL_B_SPLINE_CURVE ( ( 0.2500000000000000000, 0.2500000000000000000, 0.2500000000000000000, 0.2500000000000000000, 0.2500000000000000000, 0.2500000000000000000, 0.2500000000000000000, 0.2500000000000000000, 0.2500000000000000000, 0.2500000000000000000, 0.2500000000000000000, 0.2500000000000000000, 0.2500000000000000000, 0.2500000000000000000, 0.2500000000000000000, 0.2500000000000000000, 0.2500000000000000000, 0.2500000000000000000, 0.2500000000000000000, 0.2500000000000000000, 0.2500000000000000000, 0.2500000000000000000, 0.2500000000000000000, 0.2500000000000000000, 0.2500000000000000000, 0.2500000000000000000, 0.2500000000000000000, 0.2500000000000000000, 0.2500000000000000000, 0.2500000000000000000, 0.2500000000000000000, 0.2500000000000000000, 0.2500000000000000000, 0.2500000000000000000, 0.2500000000000000000, 0.2500000000000000000, 0.2500000000000000000, 0.2500000000000000000, 0.2500000000000000000, 0.2500000000000000000, 0.2500000000000000000, 0.2500000000000000000, 0.2500000000000000000, 0.2500000000000000000, 0.2500000000000000000, 0.2500000000000000000, 0.2500000000000000000, 0.2500000000000000000, 0.2500000000000000000, 0.2500000000000000000, 0.2500000000000000000, 0.2500000000000000000, 0.2500000000000000000, 0.2500000000000000000, 0.2500000000000000000, 0.2500000000000000000, 0.2500000000000000000, 0.2500000000000000000, 0.2500000000000000000, 0.2500000000000000000, 0.2500000000000000000, 0.2500000000000000000, 0.2500000000000000000, 0.2500000000000000000, 0.2500000000000000000, 0.2500000000000000000, 0.2500000000000000000, 0.2500000000000000000, 0.2500000000000000000, 0.2500000000000000000, 0.2500000000000000000, 0.2500000000000000000, 0.2500000000000000000, 0.2500000000000000000, 0.2500000000000000000 ) ) 
 REPRESENTATION_ITEM ( '' )  );
#9532=CARTESIAN_POINT ( 'NONE',  ( -4.368432077694425431, -0.2718166108138866943, -44.56408784452499106 ) ) ;
#9560=CARTESIAN_POINT ( 'NONE',  ( -2.158984558600606007, 5.217364672555318883, -57.14652090042499566 ) ) ;
#9597=CARTESIAN_POINT ( 'NONE',  ( -1.760169390438194759, -5.172221906152406845, -47.79520033292500614 ) ) ;
#9668=CARTESIAN_POINT ( 'NONE',  ( -4.749401372790300613, -1.581986711674698842, -68.10000000002503384 ) ) ;
#9675=CARTESIAN_POINT ( 'NONE',  ( -3.857468353316018117, 3.836780423039637178, -69.74322600342500778 ) ) ;
#9681=CARTESIAN_POINT ( 'NONE',  ( -4.050122923326508584, -2.059172231882750559, -62.36424626872499033 ) ) ;
#9710=CARTESIAN_POINT ( 'NONE',  ( -2.948077164825084306, -3.495793300896363753, -59.17407541852499975 ) ) ;
#9727=CARTESIAN_POINT ( 'NONE',  ( -0.6393421544539239498, -5.029762131177996309, -44.10000000002499121 ) ) ;
#9749=CARTESIAN_POINT ( 'NONE',  ( 4.531630834892032667, -0.6723478992683162847, -46.13818262062499542 ) ) ;
#9828=CARTESIAN_POINT ( 'NONE',  ( -4.873443905621923200, -0.09218704096741060783, -68.10000000002501963 ) ) ;
#9835=CARTESIAN_POINT ( 'NONE',  ( -0.8291470764733243071, -4.443337602648614215, -68.30745670422500382 ) ) ;
#9841=CARTESIAN_POINT ( 'NONE',  ( -1.460566089872938900, -4.291843709425553044, -46.99520033292500187 ) ) ;
#9870=CARTESIAN_POINT ( 'NONE',  ( -1.650988191866312516, 3.989749455477759721, -57.54652090042499424 ) ) ;
#9886=CARTESIAN_POINT ( 'NONE',  ( 1.017907904351449844, -4.876997505310738390, -44.10000000002499831 ) ) ;
#9894=CARTESIAN_POINT ( 'NONE',  ( -1.677440080217387219, -4.586793301645948340, -43.23640794712499513 ) ) ;
#9908=CARTESIAN_POINT ( 'NONE',  ( -6.340437944841875506, 0.6332316896323284539, -48.10737393802499184 ) ) ;
#9981=CARTESIAN_POINT ( 'NONE',  ( 0.9406167415608388538, 5.909121140422558760, -54.41500058692499664 ) ) ;
#9985=CARTESIAN_POINT ( 'NONE',  ( -4.398480579787159783, -2.501424955541164508, -68.10000000002500542 ) ) ;
#9991=CARTESIAN_POINT ( 'NONE',  ( -4.185763533044374540, 4.163314928055855901, -69.42322600472500937 ) ) ;
#9996=CARTESIAN_POINT ( 'NONE',  ( -3.948109860491266776, 2.321589337205137937, -44.84354844312500177 ) ) ;
#10028=CARTESIAN_POINT ( 'NONE',  ( -5.463799992266447525, -1.435916617982112342, -56.93102360502499693 ) ) ;
#10045=CARTESIAN_POINT ( 'NONE',  ( 2.559859836303097325, -3.484879554911406441, -44.10000000002499121 ) ) ;
#10055=CARTESIAN_POINT ( 'NONE',  ( 5.925978784015399903, -0.8792241758803844842, -45.65818262062499855 ) ) ;
#10065=CARTESIAN_POINT ( 'NONE',  ( -0.5163256777700186984, 4.538631023554798638, -48.26410749632499630 ) ) ;
#10106=CARTESIAN_POINT ( 'NONE',  ( -4.679595096517847885, 0.7234518752358163329, -44.10000000002499121 ) ) ;
#10135=CARTESIAN_POINT ( 'NONE',  ( 2.776548632478545553, -3.583402058917904753, -52.50430438132499233 ) ) ;
#10138=CARTESIAN_POINT ( 'NONE',  ( -4.438363504809300863, 1.105440681516749235, -68.10000000002499121 ) ) ;
#10181=CARTESIAN_POINT ( 'NONE',  ( -1.494970809075166329, -6.161113191638062148, -62.42311227092500303 ) ) ;
#10198=CARTESIAN_POINT ( 'NONE',  ( 2.733853777285388365, -3.446019709399517517, -44.10000000002499121 ) ) ;
#10206=CARTESIAN_POINT ( 'NONE',  ( -2.884696998040799709, 4.705809124755043982, -44.25531229042500314 ) ) ;
#10218=CARTESIAN_POINT ( 'NONE',  ( -1.572917327626556228, -4.621985533170462901, -47.74520033292501608 ) ) ;
#10292=CARTESIAN_POINT ( 'NONE',  ( 3.357378826396556271, -2.722208303779470651, -55.40923804942499942 ) ) ;
#10298=CARTESIAN_POINT ( 'NONE',  ( -4.451258330096496074, 1.095504858435497386, -68.10000000002500542 ) ) ;
#10307=CARTESIAN_POINT ( 'NONE',  ( 6.385918709370476343, 0.1527399656023400998, -63.58686508972500917 ) ) ;
#10334=CARTESIAN_POINT ( 'NONE',  ( -1.060716232127552727, -3.772072411421167892, -68.10000000002499121 ) ) ;
#10338=CARTESIAN_POINT ( 'NONE',  ( 1.672654430053971852, 5.259243695923226269, -61.26492395752499931 ) ) ;
#10353=CARTESIAN_POINT ( 'NONE',  ( 2.499815048740641199, -3.503498767398317337, -44.10000000002499121 ) ) ;
#10362=CARTESIAN_POINT ( 'NONE',  ( 2.729852257651755210, -4.492922384981882011, -45.81669147672499776 ) ) ;
#10375=CARTESIAN_POINT ( 'NONE',  ( -5.473571180597741836, 3.247285761689575168, -50.83267869292499341 ) ) ;
#10416=SURFACE_STYLE_FILL_AREA ( #27241 ) ;
#10442=CARTESIAN_POINT ( 'NONE',  ( -0.9606962270921419744, -4.447130805931738706, -55.53033560642500532 ) ) ;
#10446=CARTESIAN_POINT ( 'NONE',  ( -4.291194574663122374, 1.061632286161843020, -68.10000000002500542 ) ) ;
#10457=CARTESIAN_POINT ( 'NONE',  ( 3.415065912822992988, 4.318092861595879128, -62.83768011632499650 ) ) ;
#10486=CARTESIAN_POINT ( 'NONE',  ( 0.4200715327254807008, -3.971614891497597277, -68.10000000002499121 ) ) ;
#10492=CARTESIAN_POINT ( 'NONE',  ( -1.377718196578040954, -5.677888627607300620, -62.74311227092501753 ) ) ;
#10507=CARTESIAN_POINT ( 'NONE',  ( 2.876144609715792111, -3.506551327605733182, -44.10000000002499121 ) ) ;
#10515=CARTESIAN_POINT ( 'NONE',  ( -3.362912017748242999, 4.936852587875802278, -48.05391720692499291 ) ) ;
#10528=CARTESIAN_POINT ( 'NONE',  ( -0.9881560945370695404, 5.823346091562972227, -51.73792092402499776 ) ) ;
#10569=( NAMED_UNIT ( * ) PLANE_ANGLE_UNIT ( ) SI_UNIT ( $, .RADIAN. ) );
#10593=CARTESIAN_POINT ( 'NONE',  ( -3.735326252960651239, -2.773461810559843421, -55.52895058492500624 ) ) ;
#10598=CARTESIAN_POINT ( 'NONE',  ( -4.210742777790425606, 0.6064333458413161404, -68.10000000002500542 ) ) ;
#10605=CARTESIAN_POINT ( 'NONE',  ( 3.051761028451055680, 3.858721280585067248, -62.88768011632500077 ) ) ;
#10614=PRODUCT_DEFINITION_CONTEXT ( 'detailed design', #28867, 'design' ) ;
#10640=CARTESIAN_POINT ( 'NONE',  ( -1.078772944755383767, 5.890544393200768170, -60.73324387862499663 ) ) ;
#10654=CARTESIAN_POINT ( 'NONE',  ( 2.815684575957060343, -3.695535399317911196, -44.10000000002499121 ) ) ;
#10662=CARTESIAN_POINT ( 'NONE',  ( 5.461196134307610528, -0.8102654170096962316, -45.33818262062500537 ) ) ;
#10674=CARTESIAN_POINT ( 'NONE',  ( -3.347225659292417888, -3.617661372292495514, -50.94612412472498875 ) ) ;
#10740=CARTESIAN_POINT ( 'NONE',  ( 5.235465350887244185, -2.882605534178610984, -58.30843849682499780 ) ) ;
#10746=CARTESIAN_POINT ( 'NONE',  ( -4.164642846343869387, 0.1855225024005626999, -68.10000000002501963 ) ) ;
#10759=CARTESIAN_POINT ( 'NONE',  ( -5.001751348353093540, 2.318407806459778175, -64.97526299432499286 ) ) ;
#10782=CARTESIAN_POINT ( 'NONE',  ( 1.815007998551255941, 5.706838904126064094, -60.46492395752500215 ) ) ;
#10794=CARTESIAN_POINT ( 'NONE',  ( -3.416035461607788815, -1.991895463217535633, -44.10000000002499121 ) ) ;
#10799=CARTESIAN_POINT ( 'NONE',  ( -3.112296099710467168, 3.758517760630106785, -63.39933298492499603 ) ) ;
#10826=SURFACE_STYLE_FILL_AREA ( #12555 ) ;
#10828=CARTESIAN_POINT ( 'NONE',  ( 3.874396413951479268, -2.399869827310083803, -49.33324460762499797 ) ) ;
#10841=CARTESIAN_POINT ( 'NONE',  ( 1.728540313474559387, 5.648005006634932990, -51.46125421262499344 ) ) ;
#10903=B_SPLINE_CURVE_WITH_KNOTS ( 'NONE', 3,
 ( #3234, #5902, #22746, #12523, #10334, #24493, #893, #15504, #25110, #14900, #10486, #29976, #3544, #20387, #22134, #592, #20866, #30464, #23224, #13456, #1353, #15826, #4177, #27938, #11414, #23071, #13773, #23391, #13619, #28089, #1825, #6534, #15657, #30138, #1665, #1515, #3863, #18643, #28240, #6684, #11106, #20700, #8886, #18491, #16287, #10946, #30299, #8731, #18335, #6379, #11263, #15977, #21017, #13933, #30621, #20541, #27772, #22911, #25266, #25587, #4023, #6219, #16130, #13301, #23544, #25743, #9045, #25434, #8568, #25900, #4338, #18169, #1981, #11572, #3699, #21168, #30766, #9194, #18798, #6062, #28406, #26658, #12340, #24148, #16443, #16899, #7314, #14559, #2443, #6841, #2589, #21640, #26052, #26360, #7004, #398, #21324, #4490, #26504, #2293, #14091, #4946, #14401, #4637, #19269, #21479, #28860 ),
 .UNSPECIFIED., .F., .F.,
 ( 4, 1, 2, 2, 1, 1, 2, 2, 1, 1, 1, 2, 2, 1, 1, 1, 1, 2, 2, 1, 1, 1, 2, 2, 1, 1, 1, 1, 2, 2, 1, 1, 1, 2, 2, 1, 1, 1, 1, 2, 2, 1, 1, 1, 2, 2, 1, 1, 1, 2, 2, 1, 1, 2, 2, 1, 1, 2, 2, 1, 2, 2, 1, 2, 2, 1, 2, 2, 2, 2, 2, 4 ),
 ( 0.000000000000000000, 0.06250000000000016653, 0.09375000000000027756, 0.1250000000000003886, 0.1875000000000005274, 0.2187500000000006106, 0.2343750000000006661, 0.2500000000000006661, 0.2812500000000007772, 0.2968750000000007772, 0.3046875000000008327, 0.3085937500000008327, 0.3125000000000008327, 0.3437500000000009992, 0.3593750000000010547, 0.3671875000000011102, 0.3710937500000010547, 0.3730468750000010547, 0.3750000000000010547, 0.3906250000000009437, 0.3984375000000008882, 0.4023437500000007772, 0.4042968750000006661, 0.4062500000000005551, 0.4140625000000003886, 0.4179687500000002220, 0.4199218750000000555, 0.4208984375000000000, 0.4213867187500000000, 0.4218750000000000000, 0.4296874999999996114, 0.4335937499999994449, 0.4355468749999994449, 0.4365234374999995004, 0.4374999999999995559, 0.4453125000000000555, 0.4492187500000002776, 0.4511718750000003886, 0.4521484375000004441, 0.4526367187500004996, 0.4531250000000005551, 0.4609375000000009992, 0.4648437500000011657, 0.4667968750000012212, 0.4677734375000013323, 0.4687500000000014988, 0.4765625000000021094, 0.4804687500000023870, 0.4824218750000024980, 0.4833984375000025535, 0.4843750000000026090, 0.4921875000000026090, 0.4960937500000026090, 0.4980468750000025535, 0.5000000000000025535, 0.5156250000000015543, 0.5234375000000012212, 0.5273437500000009992, 0.5312500000000007772, 0.5468750000000004441, 0.5546875000000003331, 0.5625000000000002220, 0.5937500000000001110, 0.6093750000000002220, 0.6250000000000002220, 0.6562500000000002220, 0.6718750000000002220, 0.6875000000000002220, 0.7187500000000002220, 0.7500000000000002220, 0.8750000000000001110, 1.000000000000000000 ),
 .UNSPECIFIED. ) ;
#10905=CARTESIAN_POINT ( 'NONE',  ( -0.06606756225350368661, 5.646037861211643083, -57.31818518972499277 ) ) ;
#10920=CARTESIAN_POINT ( 'NONE',  ( -3.508509149557995421, -4.733412845326351537, -64.33409070562500176 ) ) ;
#10946=CARTESIAN_POINT ( 'NONE',  ( 2.557726607724730705, -3.485748181607284835, -68.10000000002503384 ) ) ;
#10950=CARTESIAN_POINT ( 'NONE',  ( -3.857208203705276173, -1.109566970332652946, -44.10000000002499121 ) ) ;
#10951=PLANE ( 'NONE',  #25773 ) ;
#10953=CARTESIAN_POINT ( 'NONE',  ( -4.568101251964836074, -0.2431723019727868862, -65.56421022022500722 ) ) ;
#10981=CARTESIAN_POINT ( 'NONE',  ( -0.6751951171115599948, 5.935132877056520151, -48.26410749632500341 ) ) ;
#10994=CARTESIAN_POINT ( 'NONE',  ( -3.108138112192400104, -3.359256988581868608, -50.59612412472500154 ) ) ;
#11062=CARTESIAN_POINT ( 'NONE',  ( -0.8249440165340218289, 4.504533947698903695, -59.85324387862499407 ) ) ;
#11080=CARTESIAN_POINT ( 'NONE',  ( -4.155524648305278568, -2.455537445457764978, -67.92382590962499478 ) ) ;
#11099=CARTESIAN_POINT ( 'NONE',  ( 4.390418465362644795, -3.559810858784186127, -55.40923804942499942 ) ) ;
#11106=CARTESIAN_POINT ( 'NONE',  ( 2.412651764529908593, -3.532429318983099087, -68.10000000002500542 ) ) ;
#11108=CARTESIAN_POINT ( 'NONE',  ( -4.242641152228525669, 0.8719201866695153180, -44.10000000002499831 ) ) ;
#11112=CARTESIAN_POINT ( 'NONE',  ( 5.885062339963589295, 0.1407603604956381704, -64.86686508972501031 ) ) ;
#11137=CARTESIAN_POINT ( 'NONE',  ( -5.649653782182448403, -1.974543963569185046, -49.92743646232499799 ) ) ;
#11147=CARTESIAN_POINT ( 'NONE',  ( 0.9406167415608388538, 5.909121140422558760, -54.89500058692500062 ) ) ;
#11161=FACE_OUTER_BOUND ( 'NONE', #17872, .T. ) ;
#11182=CARTESIAN_POINT ( 'NONE',  ( -2.036891525988612894, -5.569677580567498509, -43.98640794712500224 ) ) ;
#11212=CARTESIAN_POINT ( 'NONE',  ( 3.449241269337446791, -4.803451378176493591, -61.52197827312500067 ) ) ;
#11221=CARTESIAN_POINT ( 'NONE',  ( -3.393799910883221305, -2.010794396684639107, -68.10000000002500542 ) ) ;
#11229=CARTESIAN_POINT ( 'NONE',  ( -3.200877993934835075, 3.183711413074212349, -68.94322600112499799 ) ) ;
#11251=CARTESIAN_POINT ( 'NONE',  ( -4.213298386699523945, 4.800796338101376293, -53.98587006832499924 ) ) ;
#11263=CARTESIAN_POINT ( 'NONE',  ( 2.661374056126577514, -3.457594787124394831, -68.10000000002499121 ) ) ;
#11265=CARTESIAN_POINT ( 'NONE',  ( -4.322424737952120566, 1.108769406212976039, -44.10000000002499831 ) ) ;
#11268=CARTESIAN_POINT ( 'NONE',  ( 3.415065912822992988, 4.318092861595879128, -64.43768011632499793 ) ) ;
#11295=CARTESIAN_POINT ( 'NONE',  ( 4.421972129926214023, 1.961202595004077232, -51.47998794302500158 ) ) ;
#11307=CARTESIAN_POINT ( 'NONE',  ( -1.293561172433232986, -6.216321778783836294, -53.40706695232499612 ) ) ;
#11372=CARTESIAN_POINT ( 'NONE',  ( -1.231152431062140007, -5.073857922501755269, -61.19311227092500616 ) ) ;
#11381=CARTESIAN_POINT ( 'NONE',  ( -3.862012131226881806, -1.085429931028346395, -68.10000000002500542 ) ) ;
#11391=CARTESIAN_POINT ( 'NONE',  ( -5.434147616959247529, -3.211087428728324866, -68.32382590962500046 ) ) ;
#11408=CARTESIAN_POINT ( 'NONE',  ( 2.137930486642451555, 6.059703978454344941, -45.49079303332499791 ) ) ;
#11414=CARTESIAN_POINT ( 'NONE',  ( 1.880866539809174398, -3.711827103239287329, -68.10000000002501963 ) ) ;
#11418=CARTESIAN_POINT ( 'NONE',  ( -4.160135742341998899, 0.1489380525860333204, -44.10000000002499121 ) ) ;
#11424=CARTESIAN_POINT ( 'NONE',  ( 1.165515511296630446, -4.760067307266074188, -65.45397119102499062 ) ) ;
#11441=CARTESIAN_POINT ( 'NONE',  ( -1.331528626038261054, -3.699456877748816375, -44.10000000002499121 ) ) ;
#11452=CARTESIAN_POINT ( 'NONE',  ( -4.185672079393978784, 2.483218523716627768, -50.83267869292499341 ) ) ;
#11461=CARTESIAN_POINT ( 'NONE',  ( -4.803332065605933288, -2.627392435372716495, -54.14982952342499800 ) ) ;
#11496=CARTESIAN_POINT ( 'NONE',  ( -4.592700181227117540, -1.655560342997611123, -44.81497819512500058 ) ) ;
#11527=CARTESIAN_POINT ( 'NONE',  ( -0.9941633020186212422, 5.428540911361258381, -59.45324387862500259 ) ) ;
#11546=CARTESIAN_POINT ( 'NONE',  ( 4.434603606047636148, 2.142645224023219441, -66.10315453652499684 ) ) ;
#11572=CARTESIAN_POINT ( 'NONE',  ( 2.738791508839905742, -3.809105199416136234, -68.10000000002500542 ) ) ;
#11579=CARTESIAN_POINT ( 'NONE',  ( -3.807105672873282831, -5.136256491778199873, -65.61409070562500290 ) ) ;
#11603=CARTESIAN_POINT ( 'NONE',  ( 2.259239758627727745, -4.069767828330737913, -54.83172062782499268 ) ) ;
#11612=CARTESIAN_POINT ( 'NONE',  ( -1.157762119782732135, -5.359362766143966006, -56.73033560642500817 ) ) ;
#11628=ORIENTED_EDGE ( 'NONE', *, *, #1514, .F. ) ;
#11679=CARTESIAN_POINT ( 'NONE',  ( -1.078772944755383767, 5.890544393200768170, -59.77324387862499577 ) ) ;
#11696=CARTESIAN_POINT ( 'NONE',  ( 0.3196029497759475535, 5.089975830446680227, -68.87875473022501183 ) ) ;
#11722=CARTESIAN_POINT ( 'NONE',  ( -4.817157408371211424, 0.2680464973864214451, -68.10000000002500542 ) ) ;
#11754=CARTESIAN_POINT ( 'NONE',  ( -4.803332065605933288, -2.627392435372716495, -52.54982952342499658 ) ) ;
#11766=CARTESIAN_POINT ( 'NONE',  ( -1.650988191866306742, 3.989749455477753504, -57.14652090042499566 ) ) ;
#11779=APPLICATION_CONTEXT ( 'automotive_design' ) ;
#11793=CARTESIAN_POINT ( 'NONE',  ( -3.948109860491266776, 2.321589337205137937, -44.84354844312500177 ) ) ;
#11884=CARTESIAN_POINT ( 'NONE',  ( 1.257215589593053906, -4.341675124665346885, -67.70367649352500905 ) ) ;
#11887=CARTESIAN_POINT ( 'NONE',  ( -4.240613917342963113, -1.711409762446096439, -59.38491726642499202 ) ) ;
#11917=CARTESIAN_POINT ( 'NONE',  ( 4.824840617521342523, -2.656518825645647119, -59.10843849682499496 ) ) ;
#11941=CARTESIAN_POINT ( 'NONE',  ( 3.001777156698443250, -4.698362801289899693, -43.56966640442499283 ) ) ;
#11956=CARTESIAN_POINT ( 'NONE',  ( 3.389692407805913632, 3.523397910813151679, -48.69426496242499525 ) ) ;
#11999=ORIENTED_EDGE ( 'NONE', *, *, #15927, .F. ) ;
#12030=B_SPLINE_CURVE_WITH_KNOTS ( 'NONE', 3,
 ( #28243, #23547, #1518, #15661, #10794, #20389, #27941, #6064, #28094, #15830, #6687, #10950, #6536, #3867, #30624, #16132, #25747, #25268, #25905, #23226, #16289, #11418, #1668, #30141, #21021, #9050, #3703, #22915, #13305, #11108, #18645, #18339, #1356, #15981, #20704, #30301, #6383, #11265, #20869, #30467, #8891, #18496, #19703, #9355, #22217, #29287, #7728, #6844, #17482, #26777, #7877, #10106, #3014, #22069, #30769, #12308, #24580, #28565, #21920, #4641, #29444, #12451, #7007, #24426, #17334, #21328, #2861, #15129, #2135, #26940, #366, #19551, #523 ),
 .UNSPECIFIED., .F., .F.,
 ( 4, 2, 1, 1, 1, 1, 2, 2, 1, 1, 1, 1, 1, 2, 2, 1, 1, 2, 2, 1, 1, 1, 1, 2, 2, 1, 1, 2, 2, 1, 1, 1, 2, 2, 1, 1, 1, 2, 2, 1, 2, 2, 1, 2, 2, 2, 2, 2, 4 ),
 ( 0.000000000000000000, 0.1250000000000015821, 0.1875000000000024425, 0.2187500000000028588, 0.2343750000000030809, 0.2421875000000031641, 0.2460937500000032196, 0.2500000000000032752, 0.3125000000000044409, 0.3437500000000050515, 0.3593750000000053846, 0.3671875000000055511, 0.3710937500000056621, 0.3730468750000056621, 0.3750000000000057176, 0.4062500000000063283, 0.4218750000000066058, 0.4296875000000067724, 0.4375000000000069389, 0.4531250000000072720, 0.4609375000000074940, 0.4648437500000076050, 0.4667968750000076050, 0.4677734375000076050, 0.4687500000000075495, 0.4843750000000066058, 0.4921875000000061617, 0.4960937500000061062, 0.5000000000000059952, 0.5156250000000046629, 0.5234375000000037748, 0.5273437500000033307, 0.5292968750000031086, 0.5312500000000029976, 0.5468750000000023315, 0.5546875000000021094, 0.5585937500000021094, 0.5605468750000019984, 0.5625000000000018874, 0.5937500000000017764, 0.6093750000000016653, 0.6250000000000016653, 0.6562500000000015543, 0.6718750000000015543, 0.6875000000000014433, 0.7187500000000013323, 0.7500000000000011102, 0.8750000000000006661, 1.000000000000000000 ),
 .UNSPECIFIED. ) ;
#12041=CARTESIAN_POINT ( 'NONE',  ( 0.3196029497759475535, 5.089975830446680227, -69.35875473022500159 ) ) ;
#12047=CARTESIAN_POINT ( 'NONE',  ( 3.312932182603874232, 3.356011527877053702, -57.70805965152499795 ) ) ;
#12073=CARTESIAN_POINT ( 'NONE',  ( -3.855177830964256813, -4.571422008809257420, -59.65407541852500373 ) ) ;
#12088=CARTESIAN_POINT ( 'NONE',  ( -1.459689923256333843, -4.879907760210503653, -44.10000000002499121 ) ) ;
#12106=CARTESIAN_POINT ( 'NONE',  ( 5.200437648300224147, 1.853818095060352222, -46.72627377572500507 ) ) ;
#12184=CARTESIAN_POINT ( 'NONE',  ( -5.167095691178253070, 1.703695954683749125, -69.54019511502499995 ) ) ;
#12188=CARTESIAN_POINT ( 'NONE',  ( 4.692739937114380311, 0.5303478879429834869, -55.01771407622499765 ) ) ;
#12224=CARTESIAN_POINT ( 'NONE',  ( -4.072259770650454413, 2.021700601781299511, -56.79877225282499609 ) ) ;
#12247=CARTESIAN_POINT ( 'NONE',  ( 2.766343654246206984, -4.329863758072034940, -42.76966640442500989 ) ) ;
#12264=CARTESIAN_POINT ( 'NONE',  ( -4.251243323665415907, -4.132078999800212316, -47.20083066912499703 ) ) ;
#12308=CARTESIAN_POINT ( 'NONE',  ( -4.789018076886207176, 0.4073481513306022039, -44.10000000002499831 ) ) ;
#12338=CARTESIAN_POINT ( 'NONE',  ( 5.655353257550568280, 0.6391371982588460732, -54.21771407622500050 ) ) ;
#12340=CARTESIAN_POINT ( 'NONE',  ( 2.457213513335546828, -4.104727644910624029, -68.10000000002501963 ) ) ;
#12354=CARTESIAN_POINT ( 'NONE',  ( 2.994727039187461415, -3.426347720743794234, -64.49605006312501132 ) ) ;
#12382=CARTESIAN_POINT ( 'NONE',  ( 0.8945918243927786229, -4.819150861182647461, -59.14125695792499471 ) ) ;
#12397=CARTESIAN_POINT ( 'NONE',  ( 2.805604715719960840, -3.444923010881604242, -44.10000000002499121 ) ) ;
#12404=CARTESIAN_POINT ( 'NONE',  ( -1.760169390438194759, -5.172221906152406845, -46.19520033282500293 ) ) ;
#12415=CARTESIAN_POINT ( 'NONE',  ( -2.571638601809290936, 3.775240214263654526, -48.05391720702499470 ) ) ;
#12451=CARTESIAN_POINT ( 'NONE',  ( -4.892650201704735302, -0.5748897526526646207, -44.10000000002499121 ) ) ;
#12483=CARTESIAN_POINT ( 'NONE',  ( 2.964344385318878228, 3.936232207889206247, -53.87619010302499589 ) ) ;
#12488=CARTESIAN_POINT ( 'NONE',  ( -4.605309145015588079, 0.8848923369832152330, -68.10000000002499121 ) ) ;
#12501=CARTESIAN_POINT ( 'NONE',  ( 3.874396413951479268, -2.399869827310083803, -49.33324460762499797 ) ) ;
#12523=CARTESIAN_POINT ( 'NONE',  ( -1.278635117706684587, -3.697671176787224567, -68.10000000002499121 ) ) ;
#12532=CARTESIAN_POINT ( 'NONE',  ( -5.182433330280534989, 2.850054831770709285, -60.61908057272500372 ) ) ;
#12549=CARTESIAN_POINT ( 'NONE',  ( 2.604942178515098128, -3.963434524254012548, -44.10000000002500542 ) ) ;
#12555=FILL_AREA_STYLE ('',( #7979 ) ) ;
#12557=CARTESIAN_POINT ( 'NONE',  ( -2.769456955792640951, 4.065643307668772799, -47.30391720702499470 ) ) ;
#12569=CARTESIAN_POINT ( 'NONE',  ( 5.943504367937093136, -0.4395870339238064362, -49.12442242802499948 ) ) ;
#12570=ORIENTED_EDGE ( 'NONE', *, *, #22587, .F. ) ;
#12634=CARTESIAN_POINT ( 'NONE',  ( 0.8668428795416116550, 5.445660658778139762, -53.61500058692499238 ) ) ;
#12637=CARTESIAN_POINT ( 'NONE',  ( -4.204138849208283624, 0.5415514259779574679, -68.10000000002501963 ) ) ;
#12683=CARTESIAN_POINT ( 'NONE',  ( 4.009291712408949770, -2.091746824018178685, -61.31790713612500099 ) ) ;
#12698=CARTESIAN_POINT ( 'NONE',  ( 2.679732294349358668, -3.453994421436008988, -44.10000000002499121 ) ) ;
#12708=CARTESIAN_POINT ( 'NONE',  ( 1.634888019277630278, 4.633891277622259608, -45.09079303332500643 ) ) ;
#12722=CARTESIAN_POINT ( 'NONE',  ( 2.776548632478545553, -3.583402058917904753, -52.50430438132499233 ) ) ;
#12798=CARTESIAN_POINT ( 'NONE',  ( 5.235465350887244185, -2.882605534178610984, -57.82843849682499382 ) ) ;
#12804=CARTESIAN_POINT ( 'NONE',  ( -4.163090791897414711, 0.1733432904813641262, -68.10000000002503384 ) ) ;
#12817=CARTESIAN_POINT ( 'NONE',  ( 3.225090657556859419, -3.689912930009636938, -63.74605006312501132 ) ) ;
#12849=CARTESIAN_POINT ( 'NONE',  ( -4.631110635561381805, 2.546857509239208728, -60.56908057272499235 ) ) ;
#12863=CARTESIAN_POINT ( 'NONE',  ( 2.463209041803821275, -4.101496315139196547, -44.10000000002499121 ) ) ;
#12871=CARTESIAN_POINT ( 'NONE',  ( -2.571638601809289160, 3.775240214263653193, -47.65391720702500322 ) ) ;
#12883=CARTESIAN_POINT ( 'NONE',  ( 5.477347162681518000, -0.4051096195737657335, -49.92442242802499663 ) ) ;
#12951=CARTESIAN_POINT ( 'NONE',  ( -2.948077164825084306, -3.495793300896363753, -59.17407541852499975 ) ) ;
#12955=CARTESIAN_POINT ( 'NONE',  ( -4.246009911492877542, 0.8938096538029302041, -68.10000000002499121 ) ) ;
#12964=CARTESIAN_POINT ( 'NONE',  ( -5.941465883516308999, 0.03012783874251079297, -62.09122063482499243 ) ) ;
#12996=CARTESIAN_POINT ( 'NONE',  ( 5.242919931573567283, -2.735361231296036699, -61.31790713612500099 ) ) ;
#13011=CARTESIAN_POINT ( 'NONE',  ( 1.995566471097224959, -3.675172130346584964, -44.10000000002499121 ) ) ;
#13018=CARTESIAN_POINT ( 'NONE',  ( 4.315256771988541296, 1.538274589489400990, -45.52627377572500933 ) ) ;
#13030=CARTESIAN_POINT ( 'NONE',  ( -5.044271480141131470, 2.992596682328089841, -51.63267869292499768 ) ) ;
#13096=CARTESIAN_POINT ( 'NONE',  ( 5.506968775199813315, -0.09733528975458538568, -57.29793411332500597 ) ) ;
#13101=CARTESIAN_POINT ( 'NONE',  ( -4.220714658002963304, 0.7024586621993844648, -68.10000000002501963 ) ) ;
#13111=CARTESIAN_POINT ( 'NONE',  ( 3.609030021535462041, -4.129188278801706247, -63.69605006312499995 ) ) ;
#13131=CARTESIAN_POINT ( 'NONE',  ( 4.332295931058598448, 4.388630459628991787, -57.70805965152499795 ) ) ;
#13144=CARTESIAN_POINT ( 'NONE',  ( -4.543473910928012671, 0.02303893552233621245, -62.57122063472500884 ) ) ;
#13168=CARTESIAN_POINT ( 'NONE',  ( 3.650437977654107602, 3.794428519304413605, -47.94426496242498814 ) ) ;
#13179=CARTESIAN_POINT ( 'NONE',  ( 5.066518387468507356, -3.138291312573631586, -49.81324460762500195 ) ) ;
#13249=CARTESIAN_POINT ( 'NONE',  ( 3.312932182603870679, 3.356011527877057254, -57.30805965152501358 ) ) ;
#13271=CARTESIAN_POINT ( 'NONE',  ( -4.069925668896384963, 4.914984763948436530, -62.51933298482501300 ) ) ;
#13294=CARTESIAN_POINT ( 'NONE',  ( -0.6751951171170902377, 5.935132877048193478, -48.26410749642499809 ) ) ;
#13301=CARTESIAN_POINT ( 'NONE',  ( 2.876615514287123254, -3.533536248196276652, -68.10000000002499121 ) ) ;
#13305=CARTESIAN_POINT ( 'NONE',  ( -4.237596627851885067, 0.8380315630058113863, -44.10000000002499121 ) ) ;
#13308=CARTESIAN_POINT ( 'NONE',  ( 5.384875807261761516, 2.601783486389667832, -66.85315453642499506 ) ) ;
#13334=CARTESIAN_POINT ( 'NONE',  ( 0.8648632234848976363, -6.342619565911398638, -49.76468436622499780 ) ) ;
#13347=CARTESIAN_POINT ( 'NONE',  ( 1.321824945545745145, 4.319062652178982553, -51.46125421262499344 ) ) ;
#13410=CARTESIAN_POINT ( 'NONE',  ( 4.569612387855602087, -0.08076758077263379576, -58.09793411332499602 ) ) ;
#13426=CARTESIAN_POINT ( 'NONE',  ( 1.304267357867700872, -5.326741986711696519, -63.90397119102498635 ) ) ;
#13456=CARTESIAN_POINT ( 'NONE',  ( 1.338051363053742282, -3.857864915027613861, -68.10000000002501963 ) ) ;
#13462=CARTESIAN_POINT ( 'NONE',  ( 6.385918709370476343, 0.1527399656023400998, -64.06686508972499894 ) ) ;
#13489=CARTESIAN_POINT ( 'NONE',  ( 5.066518387468507356, -3.138291312573631586, -48.85324460762499399 ) ) ;
#13502=CARTESIAN_POINT ( 'NONE',  ( 0.7192951553254730568, 4.518739695583319893, -54.81500058692499522 ) ) ;
#13540=CARTESIAN_POINT ( 'NONE',  ( 3.001777156698443250, -4.698362801289899693, -44.04966640442499681 ) ) ;
#13574=CARTESIAN_POINT ( 'NONE',  ( 3.178712542294670040, -4.426710093576285310, -60.72197827312499641 ) ) ;
#13593=CARTESIAN_POINT ( 'NONE',  ( 4.441146713721671802, -1.990734395214990071, -67.27841551502500295 ) ) ;
#13610=CARTESIAN_POINT ( 'NONE',  ( 3.314820598666778917, -5.455691467570147779, -46.56669147682499954 ) ) ;
#13619=CARTESIAN_POINT ( 'NONE',  ( 2.029564108346094908, -3.664007903844075820, -68.10000000002500542 ) ) ;
#13626=CARTESIAN_POINT ( 'NONE',  ( 3.705709820302785396, 4.685590126413917034, -63.63768011632500787 ) ) ;
#13651=CARTESIAN_POINT ( 'NONE',  ( -5.473571180597741836, 3.247285761689575168, -50.83267869292499341 ) ) ;
#13661=CARTESIAN_POINT ( 'NONE',  ( 3.317242526498128008, 4.404831280267538673, -55.42619010302500016 ) ) ;
#13700=CARTESIAN_POINT ( 'NONE',  ( -1.557622931652903331, -4.259165208650873780, -44.38640794712500792 ) ) ;
#13728=CARTESIAN_POINT ( 'NONE',  ( -5.296314592117303377, -2.692763687817543161, -61.88424626872500056 ) ) ;
#13746=CARTESIAN_POINT ( 'NONE',  ( 1.644051155559919764, -5.677575162961061572, -67.70367649352500905 ) ) ;
#13763=CARTESIAN_POINT ( 'NONE',  ( 5.943504367937093136, -0.4395870339238064362, -49.12442242802499948 ) ) ;
#13773=CARTESIAN_POINT ( 'NONE',  ( 1.905093263558854666, -3.704216562065955731, -68.10000000002500542 ) ) ;
#13780=CARTESIAN_POINT ( 'NONE',  ( 2.833778097863427714, 3.583098331959792660, -63.63768011632500787 ) ) ;
#13808=CARTESIAN_POINT ( 'NONE',  ( -3.347225659292417888, -3.617661372292495514, -49.44612412472500296 ) ) ;
#13820=CARTESIAN_POINT ( 'NONE',  ( 2.752605500610146638, 3.655072764496610560, -55.02619010302499447 ) ) ;
#13827=COLOUR_RGB ( '', 0.31764706, 0.68627451, 0.89019608) ;
#13859=CARTESIAN_POINT ( 'NONE',  ( -5.534792526179823646, -1.995162464570431782, -45.21497819512499916 ) ) ;
#13889=CARTESIAN_POINT ( 'NONE',  ( -1.494970809075166329, -6.161113191638062148, -61.46311227092499507 ) ) ;
#13907=CARTESIAN_POINT ( 'NONE',  ( -3.200877993934844401, 3.183711413074225671, -68.54322600212499594 ) ) ;
#13927=CARTESIAN_POINT ( 'NONE',  ( -1.494970809075166329, -6.161113191638062148, -61.94311227092499195 ) ) ;
#13933=CARTESIAN_POINT ( 'NONE',  ( 2.739374102630459884, -3.445395115450355483, -68.10000000002501963 ) ) ;
#13941=CARTESIAN_POINT ( 'NONE',  ( -2.911316102860724175, -3.927725552502973727, -65.13409070562501313 ) ) ;
#13968=CARTESIAN_POINT ( 'NONE',  ( 2.097865490181829884, -3.779070126327673140, -55.58172062782499268 ) ) ;
#13977=CARTESIAN_POINT ( 'NONE',  ( 6.136659917679837761, 0.6935318534637759935, -55.01771407622499765 ) ) ;
#14015=DIRECTION ( 'NONE',  ( 0.000000000000000000, 0.000000000000000000, 1.000000000000000000 ) ) ;
#14018=FACE_OUTER_BOUND ( 'NONE', #1156, .T. ) ;
#14049=CARTESIAN_POINT ( 'NONE',  ( 4.508719565894415915, 1.847421675581904843, -60.89141554682500157 ) ) ;
#14065=CARTESIAN_POINT ( 'NONE',  ( 0.2444022557069394641, 3.892334458579130185, -69.35875473022500159 ) ) ;
#14085=CARTESIAN_POINT ( 'NONE',  ( -4.069925668896384963, 4.914984763948436530, -62.99933298482500277 ) ) ;
#14091=CARTESIAN_POINT ( 'NONE',  ( 0.3358324584398617585, -5.008269611061795246, -68.10000000002501963 ) ) ;
#14099=CARTESIAN_POINT ( 'NONE',  ( -1.895255389310859684, 5.229048247678121264, -69.15099036452500059 ) ) ;
#14121=CARTESIAN_POINT ( 'NONE',  ( -0.9606962270921406422, -4.447130805931738706, -55.93033560642499680 ) ) ;
#14133=CARTESIAN_POINT ( 'NONE',  ( 0.8668428795360779704, 5.445660658769813089, -55.21500058692499380 ) ) ;
#14156=CARTESIAN_POINT ( 'NONE',  ( -6.005838698572866008, -2.164963525412170853, -44.41497819512499490 ) ) ;
#14170=CARTESIAN_POINT ( 'NONE',  ( -2.577814338686791107, 4.205191132749348526, -45.80531229042500030 ) ) ;
#14259=CARTESIAN_POINT ( 'NONE',  ( -2.911316102860724175, -3.927725552502973727, -65.13409070562501313 ) ) ;
#14290=CARTESIAN_POINT ( 'NONE',  ( 4.569612387855602087, -0.08076758077263958280, -58.49793411332501591 ) ) ;
#14335=CARTESIAN_POINT ( 'NONE',  ( -3.099154212379724882, 4.549648463301534385, -48.85391720692500428 ) ) ;
#14401=CARTESIAN_POINT ( 'NONE',  ( -0.4042037169903076044, -5.063438148506004488, -68.10000000002501963 ) ) ;
#14409=CARTESIAN_POINT ( 'NONE',  ( 1.515105966933908421, -5.232275150211489922, -68.50367649352499200 ) ) ;
#14414=CARTESIAN_POINT ( 'NONE',  ( 4.421972129926212247, 1.961202595004083005, -51.87998794302499306 ) ) ;
#14445=CARTESIAN_POINT ( 'NONE',  ( 0.9634065801723908917, -5.189854773623245876, -59.49125695792500323 ) ) ;
#14471=CARTESIAN_POINT ( 'NONE',  ( -6.005838698572866008, -2.164963525412170853, -43.93497819512499802 ) ) ;
#14483=CARTESIAN_POINT ( 'NONE',  ( 5.461196134307610528, -0.8102654170096962316, -46.93818262062499969 ) ) ;
#14497=CARTESIAN_POINT ( 'NONE',  ( -2.744417411265728912, -4.298957096598221561, -44.10000000002499121 ) ) ;
#14559=CARTESIAN_POINT ( 'NONE',  ( 2.184925289844788399, -4.318546512737748699, -68.10000000002500542 ) ) ;
#14560=CARTESIAN_POINT ( 'NONE',  ( -4.894918280844120950, -0.4876114613646642115, -68.10000000002500542 ) ) ;
#14566=CARTESIAN_POINT ( 'NONE',  ( 1.353924481083393028, -4.675650134241364775, -68.45367649352499484 ) ) ;
#14573=CARTESIAN_POINT ( 'NONE',  ( 4.003591150705129387, -2.204345408526039218, -58.30843849682500490 ) ) ;
#14602=CARTESIAN_POINT ( 'NONE',  ( -5.623491485972666126, 3.092612689740418919, -59.81908057272499946 ) ) ;
#14616=CARTESIAN_POINT ( 'NONE',  ( -0.07854999671243234616, -5.046990879750716807, -44.10000000002500542 ) ) ;
#14623=CARTESIAN_POINT ( 'NONE',  ( 2.295476649252891743, -3.592865671589301257, -43.16966640442500847 ) ) ;
#14637=CARTESIAN_POINT ( 'NONE',  ( 4.315256771988541296, 1.538274589489400990, -46.32627377572500649 ) ) ;
#14705=CARTESIAN_POINT ( 'NONE',  ( 3.630871288588910506, -4.685987307826644965, -52.50430438132499944 ) ) ;
#14715=CARTESIAN_POINT ( 'NONE',  ( -4.287590041606506475, 1.413705153860729924, -69.14019511502500848 ) ) ;
#14719=CARTESIAN_POINT ( 'NONE',  ( -1.143212971672622036, -4.711439499498762729, -61.94311227092499195 ) ) ;
#14749=CARTESIAN_POINT ( 'NONE',  ( 3.312932182603870679, 3.356011527877057254, -58.10805965152499653 ) ) ;
#14765=CARTESIAN_POINT ( 'NONE',  ( 1.983129573338659579, -3.679247247662226883, -44.10000000002498410 ) ) ;
#14772=CARTESIAN_POINT ( 'NONE',  ( -0.6222386373588042474, 5.469632259241050676, -47.46410749632500625 ) ) ;
#14787=CARTESIAN_POINT ( 'NONE',  ( -2.571638601809289160, 3.775240214263653193, -48.45391720702500749 ) ) ;
#14838=( LENGTH_UNIT ( ) NAMED_UNIT ( * ) SI_UNIT ( .MILLI., .METRE. ) );
#14865=CARTESIAN_POINT ( 'NONE',  ( -4.213298386699523945, 4.800796338101376293, -53.98587006832499924 ) ) ;
#14868=CARTESIAN_POINT ( 'NONE',  ( -4.579986235535789874, 0.9295504054295574692, -68.10000000002499121 ) ) ;
#14882=CARTESIAN_POINT ( 'NONE',  ( -3.108138112192390778, -3.359256988581870385, -50.19612412472499585 ) ) ;
#14900=CARTESIAN_POINT ( 'NONE',  ( 0.3030197492349069321, -3.973671256962546749, -68.10000000002499121 ) ) ;
#14906=CARTESIAN_POINT ( 'NONE',  ( 1.169850847344618083, -6.301966510834352775, -59.22125695792499300 ) ) ;
#14922=CARTESIAN_POINT ( 'NONE',  ( 2.613626818191559398, -3.470008059885128837, -44.10000000002499121 ) ) ;
#14929=CARTESIAN_POINT ( 'NONE',  ( -2.393684743089945055, 3.904820337558672083, -44.65531229042500172 ) ) ;
#14940=CARTESIAN_POINT ( 'NONE',  ( -3.501023913647623331, -3.402888588040827500, -47.95083066912501124 ) ) ;
#15005=B_SPLINE_CURVE_WITH_KNOTS ( 'NONE', 3,
 ( #21697, #16650, #5008, #6896, #26567, #24061, #12088, #146, #9727, #14616, #21857, #308, #9886, #19488, #23755, #3258, #29845, #20245, #917, #15072, #24364, #12863, #26716, #17422, #2955, #12549, #3409, #5318, #5774, #17574, #463, #10654, #24518, #3102, #1063, #5619, #2805, #612, #27029, #10507, #22007, #19945, #17115, #12397, #5465, #24668, #22155, #10198, #19798, #12698, #29383, #14922, #22310, #24824, #762, #10045, #10353, #5152, #22465, #29539, #7973, #7823, #27180, #20107, #13011, #15219, #29695, #14765, #8122, #15376, #19639, #17717, #29225, #27335, #24973, #22623, #7665, #17268, #26877, #1537, #18029, #18364, #30159, #25767, #27797, #8431, #11441, #23095, #17873 ),
 .UNSPECIFIED., .F., .F.,
 ( 4, 2, 2, 2, 2, 2, 2, 1, 1, 2, 2, 1, 1, 1, 1, 2, 2, 1, 1, 1, 2, 2, 2, 2, 2, 2, 1, 1, 2, 2, 1, 1, 1, 2, 2, 1, 2, 2, 1, 1, 1, 1, 2, 2, 1, 1, 2, 2, 1, 1, 2, 2, 1, 1, 2, 2, 4 ),
 ( 0.000000000000000000, 0.03125000000000302536, 0.06250000000000605072, 0.1250000000000121569, 0.1875000000000182632, 0.2500000000000243694, 0.3125000000000304756, 0.3437500000000335287, 0.3593750000000350830, 0.3671875000000358602, 0.3750000000000366929, 0.4062500000000395795, 0.4218750000000410227, 0.4296875000000416889, 0.4335937500000420775, 0.4355468750000421885, 0.4375000000000422440, 0.4531250000000427991, 0.4609375000000430767, 0.4648437500000431877, 0.4667968750000431877, 0.4687500000000431877, 0.4765625000000434097, 0.4843750000000436318, 0.4921875000000437983, 0.5000000000000439648, 0.5078125000000442979, 0.5117187500000442979, 0.5136718750000442979, 0.5156250000000442979, 0.5234375000000442979, 0.5273437500000444089, 0.5292968750000445199, 0.5302734375000445199, 0.5312500000000446310, 0.5468750000000431877, 0.5546875000000425215, 0.5625000000000417444, 0.5781250000000404121, 0.5859375000000397460, 0.5898437500000394129, 0.5917968750000394129, 0.5927734375000394129, 0.5937500000000394129, 0.6093750000000378586, 0.6171875000000370814, 0.6210937500000367484, 0.6250000000000363043, 0.6875000000000303091, 0.7187500000000274225, 0.7343750000000258682, 0.7500000000000244249, 0.8125000000000183187, 0.8437500000000153211, 0.8593750000000137668, 0.8750000000000123235, 1.000000000000000000 ),
 .UNSPECIFIED. ) ;
#15011=CARTESIAN_POINT ( 'NONE',  ( -0.9891938378274525157, -4.753657830815115837, -52.92706695232499925 ) ) ;
#15017=CARTESIAN_POINT ( 'NONE',  ( -4.718533212916164565, 0.6243469615916787951, -68.10000000002501963 ) ) ;
#15030=CARTESIAN_POINT ( 'NONE',  ( -0.9769741165347872736, -4.003510540716011867, -67.93704710652500012 ) ) ;
#15058=CARTESIAN_POINT ( 'NONE',  ( -3.112296099710462727, 3.758517760630103233, -62.99933298492499034 ) ) ;
#15072=CARTESIAN_POINT ( 'NONE',  ( 2.128921717830389859, -4.360192604088349633, -44.10000000002499831 ) ) ;
#15080=CARTESIAN_POINT ( 'NONE',  ( -4.251243323665415907, -4.132078999800212316, -46.72083066912499305 ) ) ;
#15094=CARTESIAN_POINT ( 'NONE',  ( 5.782578939028539367, 2.564649547393091478, -51.87998794302499306 ) ) ;
#15129=CARTESIAN_POINT ( 'NONE',  ( -4.766028791791773855, -1.519250813530571564, -44.10000000002499121 ) ) ;
#15156=CARTESIAN_POINT ( 'NONE',  ( -0.05052225346893526176, 4.317558364482406930, -56.91818518972499419 ) ) ;
#15159=CARTESIAN_POINT ( 'NONE',  ( -4.680684891358993127, 0.7214394727549908737, -68.10000000002501963 ) ) ;
#15169=CARTESIAN_POINT ( 'NONE',  ( -5.427432314178970429, 2.515719109140460041, -65.29526299442500203 ) ) ;
#15204=CARTESIAN_POINT ( 'NONE',  ( 0.8372177269581546621, 4.490875019823945991, -63.42744533512499316 ) ) ;
#15219=CARTESIAN_POINT ( 'NONE',  ( 1.988743700875508891, -3.677409591406694211, -44.10000000002499121 ) ) ;
#15228=CARTESIAN_POINT ( 'NONE',  ( -4.251243323665415907, -4.132078999800212316, -47.20083066912499703 ) ) ;
#15238=CARTESIAN_POINT ( 'NONE',  ( 4.416651415012724513, -2.079980245798425109, -53.04872167392500870 ) ) ;
#15284=SURFACE_SIDE_STYLE ('',( #10416 ) ) ;
#15315=CARTESIAN_POINT ( 'NONE',  ( 0.8945918243927832858, -4.819150861182647461, -58.74125695792500323 ) ) ;
#15320=CARTESIAN_POINT ( 'NONE',  ( -4.222785574039375156, 0.7211312973832428863, -68.10000000002500542 ) ) ;
#15330=CARTESIAN_POINT ( 'NONE',  ( 5.885062339963589295, 0.1407603604956381704, -63.26686508972500178 ) ) ;
#15333=CARTESIAN_POINT ( 'NONE',  ( -2.098441946322436635, -3.287561928151557122, -68.10000000002500542 ) ) ;
#15363=CARTESIAN_POINT ( 'NONE',  ( 5.433585117924402574, 2.226379967917181180, -61.69141554682499873 ) ) ;
#15376=CARTESIAN_POINT ( 'NONE',  ( 1.851108483524190662, -3.721478854253624124, -44.10000000002499121 ) ) ;
#15382=CARTESIAN_POINT ( 'NONE',  ( 2.534862810676351330, -4.171999357468123115, -46.16669147672499918 ) ) ;
#15395=CARTESIAN_POINT ( 'NONE',  ( -0.7556487780321456960, 4.453147011089717111, -51.65792092402499947 ) ) ;
#15463=CARTESIAN_POINT ( 'NONE',  ( 4.311559700750661861, -2.373910439939187267, -57.55843849682501201 ) ) ;
#15471=CARTESIAN_POINT ( 'NONE',  ( -4.224014620368086170, 0.7320701895516892321, -68.10000000002501963 ) ) ;
#15482=CARTESIAN_POINT ( 'NONE',  ( 2.833778097863427714, 3.583098331959792660, -63.63768011632500787 ) ) ;
#15484=CARTESIAN_POINT ( 'NONE',  ( 1.891787376696312029, -3.825877967903179577, -67.61367454182500580 ) ) ;
#15498=CARTESIAN_POINT ( 'NONE',  ( -5.162912894389027230, 3.035924517800103750, -44.84354844312500177 ) ) ;
#15504=CARTESIAN_POINT ( 'NONE',  ( -0.2758148021258401417, -3.950156389878017649, -68.10000000002503384 ) ) ;
#15509=CARTESIAN_POINT ( 'NONE',  ( -1.231152431062140007, -5.073857922501755269, -62.69311227092499905 ) ) ;
#15533=CARTESIAN_POINT ( 'NONE',  ( -5.044271480141131470, 2.992596682328089841, -50.03267869292500336 ) ) ;
#15545=CARTESIAN_POINT ( 'NONE',  ( -4.064488300603595228, -4.392874523441014034, -50.67612412472499983 ) ) ;
#15616=CARTESIAN_POINT ( 'NONE',  ( 5.975646968830259809, -0.1056191442178888718, -58.09793411332499602 ) ) ;
#15630=CARTESIAN_POINT ( 'NONE',  ( -1.313688977135577529, 5.115945099120181361, -65.45876360982501296 ) ) ;
#15649=CARTESIAN_POINT ( 'NONE',  ( 5.066518387468507356, -3.138291312573631586, -49.33324460762499797 ) ) ;
#15657=CARTESIAN_POINT ( 'NONE',  ( 2.229356664414377853, -3.595762368830520916, -68.10000000002503384 ) ) ;
#15661=CARTESIAN_POINT ( 'NONE',  ( -3.221943696565561677, -2.259922541635331239, -44.10000000002498410 ) ) ;
#15664=CARTESIAN_POINT ( 'NONE',  ( 5.896017893897736784, 2.415859114112482775, -60.89141554682500157 ) ) ;
#15687=CARTESIAN_POINT ( 'NONE',  ( -4.185672079393965461, 2.483218523716621107, -50.43267869292500194 ) ) ;
#15697=CARTESIAN_POINT ( 'NONE',  ( 1.321824945545741814, 4.319062652178985218, -51.86125421262499202 ) ) ;
#15773=CARTESIAN_POINT ( 'NONE',  ( -2.158984558600606007, 5.217364672555318883, -56.66652090042499879 ) ) ;
#15793=CARTESIAN_POINT ( 'NONE',  ( -4.568101251964836074, -0.2431723019727868862, -65.56421022022500722 ) ) ;
#15794=ADVANCED_FACE ( 'NONE', ( #11161 ), #20757, .F. ) ;
#15819=CARTESIAN_POINT ( 'NONE',  ( 3.630871288588910506, -4.685987307826644965, -52.50430438132499944 ) ) ;
#15826=CARTESIAN_POINT ( 'NONE',  ( 1.704635467467862764, -3.764872627205382738, -68.10000000002499121 ) ) ;
#15830=CARTESIAN_POINT ( 'NONE',  ( -3.764950641351794136, -1.323627178738328913, -44.10000000002499121 ) ) ;
#15834=CARTESIAN_POINT ( 'NONE',  ( 1.415268835070086828, -5.780081730205603563, -65.18397119102500881 ) ) ;
#15859=CARTESIAN_POINT ( 'NONE',  ( 5.943504367937093136, -0.4395870339238064362, -48.64442242802499550 ) ) ;
#15871=CARTESIAN_POINT ( 'NONE',  ( -3.735326252960651239, -2.773461810559843421, -57.02895058492501335 ) ) ;
#15904=CARTESIAN_POINT ( 'NONE',  ( 3.915051063684143795, -2.600456723069958453, -44.15875473022499875 ) ) ;
#15927=EDGE_CURVE ( 'NONE', #3457, #5941, #15005, .T. ) ;
#15933=CARTESIAN_POINT ( 'NONE',  ( 4.831710525212951524, -2.520823095555479565, -60.51790713612500383 ) ) ;
#15951=CARTESIAN_POINT ( 'NONE',  ( -4.287590041606510916, 1.413705153860731034, -68.74019511502500279 ) ) ;
#15977=CARTESIAN_POINT ( 'NONE',  ( 2.708282711769271156, -3.449188895666643884, -68.10000000002501963 ) ) ;
#15981=CARTESIAN_POINT ( 'NONE',  ( -4.246760801282904119, 0.8971541554341054825, -44.10000000002499121 ) ) ;
#15984=CARTESIAN_POINT ( 'NONE',  ( -1.313688977135577529, 5.115945099120181361, -66.95876360972499697 ) ) ;
#16010=CARTESIAN_POINT ( 'NONE',  ( 1.321824945545741814, 4.319062652178985218, -51.06125421262500197 ) ) ;
#16020=CARTESIAN_POINT ( 'NONE',  ( 0.7746255519259798161, 4.866335056765463740, -55.16500058692498953 ) ) ;
#16059=CARTESIAN_POINT ( 'NONE',  ( 2.295476649252899293, -3.592865671589305698, -43.56966640442499994 ) ) ;
#16088=CARTESIAN_POINT ( 'NONE',  ( -4.050122923326521018, -2.059172231882739457, -61.96424626872499175 ) ) ;
#16106=CARTESIAN_POINT ( 'NONE',  ( 4.962532606730165163, 2.397722036441031435, -66.05315453652499968 ) ) ;
#16124=CARTESIAN_POINT ( 'NONE',  ( 0.8648632234848976363, -6.342619565911398638, -49.76468436622499780 ) ) ;
#16130=CARTESIAN_POINT ( 'NONE',  ( 2.876789788197821718, -3.528003781030157437, -68.10000000002500542 ) ) ;
#16132=CARTESIAN_POINT ( 'NONE',  ( -4.111734365088209664, -0.1631247855115738887, -44.10000000002499121 ) ) ;
#16136=CARTESIAN_POINT ( 'NONE',  ( 5.807653394784360934, -2.603268055249425394, -67.27841551502500295 ) ) ;
#16162=CARTESIAN_POINT ( 'NONE',  ( -4.064488300603595228, -4.392874523441014034, -50.19612412472499585 ) ) ;
#16173=CARTESIAN_POINT ( 'NONE',  ( -0.9891938378274514054, -4.753657830815118501, -53.32706695232499783 ) ) ;
#16239=CARTESIAN_POINT ( 'NONE',  ( 2.637655088286928962, -3.673227524439524050, -61.52197827312500067 ) ) ;
#16256=CARTESIAN_POINT ( 'NONE',  ( -5.007939960741254026, -2.959237434304809788, -67.52382590962501752 ) ) ;
#16287=CARTESIAN_POINT ( 'NONE',  ( 2.536848156347102368, -3.492023641679737000, -68.10000000002503384 ) ) ;
#16289=CARTESIAN_POINT ( 'NONE',  ( -4.140705449094239654, 0.009913425260839086456, -44.10000000002497700 ) ) ;
#16293=CARTESIAN_POINT ( 'NONE',  ( 5.352151167818264277, -2.399090168609281370, -68.07841551502500010 ) ) ;
#16319=CARTESIAN_POINT ( 'NONE',  ( 4.390418465362644795, -3.559810858784186127, -55.40923804942499942 ) ) ;
#16331=CARTESIAN_POINT ( 'NONE',  ( 2.743362564037614248, -4.941860934411918649, -55.58172062782499268 ) ) ;
#16366=CARTESIAN_POINT ( 'NONE',  ( -4.251810618965843780, 2.500173132353668226, -45.59354844312499466 ) ) ;
#16399=CARTESIAN_POINT ( 'NONE',  ( -5.182433330280534989, 2.850054831770709285, -59.01908057272500230 ) ) ;
#16415=CARTESIAN_POINT ( 'NONE',  ( -1.449312944839797890, 3.998683954144016894, -69.15099036452500059 ) ) ;
#16443=CARTESIAN_POINT ( 'NONE',  ( 2.333807673937585925, -4.208960876372860760, -68.10000000002503384 ) ) ;
#16449=CARTESIAN_POINT ( 'NONE',  ( 1.644051155559919764, -5.677575162961061572, -68.18367649352499882 ) ) ;
#16471=CARTESIAN_POINT ( 'NONE',  ( -4.541600168151706640, -0.1148504950298593758, -53.15673954922500144 ) ) ;
#16480=CARTESIAN_POINT ( 'NONE',  ( -0.9606962270921406422, -4.447130805931738706, -55.93033560642499680 ) ) ;
#16520=CARTESIAN_POINT ( 'NONE',  ( -1.877135327876712667, -5.132840123261955156, -44.78640794712499940 ) ) ;
#16567=CARTESIAN_POINT ( 'NONE',  ( 0.2945360517547964130, 4.690762039826936736, -68.55875473022499023 ) ) ;
#16592=CARTESIAN_POINT ( 'NONE',  ( -4.854067883769174863, 0.05624032484770506712, -68.10000000002500542 ) ) ;
#16599=CARTESIAN_POINT ( 'NONE',  ( -5.606848515966891711, 1.848691355091094835, -69.22019511502500677 ) ) ;
#16605=CARTESIAN_POINT ( 'NONE',  ( 1.387947292976102087, 4.364053279572885025, -60.46492395752500215 ) ) ;
#16624=CARTESIAN_POINT ( 'NONE',  ( 4.942443250116775211, -2.327596941721505441, -51.49872167392499733 ) ) ;
#16633=CARTESIAN_POINT ( 'NONE',  ( -2.948077164825098517, -3.495793300896359312, -59.57407541852499833 ) ) ;
#16650=CARTESIAN_POINT ( 'NONE',  ( -2.624330064346227509, -4.375605581812514799, -44.10000000002499121 ) ) ;
#16656=CARTESIAN_POINT ( 'NONE',  ( -4.945984810541346199, -1.782911138613007207, -43.66497819512500200 ) ) ;
#16671=CARTESIAN_POINT ( 'NONE',  ( -3.917812474729757799, -3.807994372373406211, -48.00083066912500129 ) ) ;
#16751=CARTESIAN_POINT ( 'NONE',  ( 1.644051155559919764, -5.677575162961061572, -67.70367649352500905 ) ) ;
#16757=CARTESIAN_POINT ( 'NONE',  ( -3.985743628842679076, -2.180176701716177057, -53.34982952342500084 ) ) ;
#16788=CARTESIAN_POINT ( 'NONE',  ( -5.325262776965995926, 2.643762325383679279, -57.27877225282499296 ) ) ;
#16831=CARTESIAN_POINT ( 'NONE',  ( -0.6751951171115599948, 5.935132877056520151, -48.74410749642499496 ) ) ;
#16899=CARTESIAN_POINT ( 'NONE',  ( 2.260959825389143862, -4.263672264598562300, -68.10000000002500542 ) ) ;
#16910=CARTESIAN_POINT ( 'NONE',  ( -0.7556487780321572423, 4.453147011089724217, -51.25792092402500089 ) ) ;
#16944=CARTESIAN_POINT ( 'NONE',  ( 3.312932182603874232, 3.356011527877053702, -57.70805965152499795 ) ) ;
#16985=CARTESIAN_POINT ( 'NONE',  ( 5.643028086411650435, 2.011589847869324377, -45.92627377572500080 ) ) ;
#17065=CARTESIAN_POINT ( 'NONE',  ( -3.200877993934835075, 3.183711413074212349, -68.94322600112499799 ) ) ;
#17071=CARTESIAN_POINT ( 'NONE',  ( -0.9606962270921406422, -4.447130805931738706, -55.93033560642499680 ) ) ;
#17100=CARTESIAN_POINT ( 'NONE',  ( -4.385510522249749243, 2.177216032696348780, -57.54877225282500319 ) ) ;
#17115=CARTESIAN_POINT ( 'NONE',  ( 2.828562571734781095, -3.451486673425649077, -44.10000000002499831 ) ) ;
#17134=CARTESIAN_POINT ( 'NONE',  ( 5.925978784015399903, -0.8792241758803844842, -46.61818262062499940 ) ) ;
#17203=CARTESIAN_POINT ( 'NONE',  ( -1.192105394233154314, -5.728767129463715690, -52.12706695232498788 ) ) ;
#17208=CARTESIAN_POINT ( 'NONE',  ( -4.117519161151379059, -0.1404918132599033975, -68.10000000002499121 ) ) ;
#17219=CARTESIAN_POINT ( 'NONE',  ( 2.637655088286928962, -3.673227524439524050, -61.52197827312500067 ) ) ;
#17248=CARTESIAN_POINT ( 'NONE',  ( -0.05440858064702409902, 4.649678238646714590, -58.06818518972500698 ) ) ;
#17268=CARTESIAN_POINT ( 'NONE',  ( 0.5885947091413640253, -3.963556596990289727, -44.10000000002499831 ) ) ;
#17276=CARTESIAN_POINT ( 'NONE',  ( -3.501023913647623331, -3.402888588040827500, -46.45083066912499703 ) ) ;
#17292=CARTESIAN_POINT ( 'NONE',  ( 4.880217822150678231, -0.7240669684095875080, -46.88818262062500963 ) ) ;
#17309=EDGE_CURVE ( 'NONE', #3457, #29133, #9517, .T. ) ;
#17334=CARTESIAN_POINT ( 'NONE',  ( -4.865310089958662765, -0.9828511995358047981, -44.10000000002499121 ) ) ;
#17361=CARTESIAN_POINT ( 'NONE',  ( -5.473210459063365896, -0.1384095708982860384, -52.75673954922498865 ) ) ;
#17364=CARTESIAN_POINT ( 'NONE',  ( -4.747698592653731176, 0.5343720360068521247, -68.10000000002500542 ) ) ;
#17405=CARTESIAN_POINT ( 'NONE',  ( -4.069925668896384963, 4.914984763948436530, -62.99933298482500277 ) ) ;
#17422=CARTESIAN_POINT ( 'NONE',  ( 2.578787959589605716, -3.990362813461365121, -44.10000000002499121 ) ) ;
#17431=CARTESIAN_POINT ( 'NONE',  ( 5.643028086411650435, 2.011589847869324377, -45.92627377572500080 ) ) ;
#17442=CARTESIAN_POINT ( 'NONE',  ( 2.990129296507525680, -3.859048371143013245, -53.25430438132500655 ) ) ;
#17482=CARTESIAN_POINT ( 'NONE',  ( -4.602032322722164892, 0.8949949322525938555, -44.10000000002499831 ) ) ;
#17487=( NAMED_UNIT ( * ) PLANE_ANGLE_UNIT ( ) SI_UNIT ( $, .RADIAN. ) );
#17513=CARTESIAN_POINT ( 'NONE',  ( -5.325262776966551037, 2.643762325382846612, -56.79877225282499609 ) ) ;
#17519=CARTESIAN_POINT ( 'NONE',  ( -4.207018160331792878, 0.5698972141343202624, -68.10000000002500542 ) ) ;
#17526=CARTESIAN_POINT ( 'NONE',  ( -3.112296099710467168, 3.758517760630106785, -62.59933298492499887 ) ) ;
#17530=CARTESIAN_POINT ( 'NONE',  ( 4.117846205589234643, 1.989599136607407504, -66.85315453642499506 ) ) ;
#17559=CARTESIAN_POINT ( 'NONE',  ( 4.508719565894404369, 1.847421675581905953, -61.29141554682499304 ) ) ;
#17574=CARTESIAN_POINT ( 'NONE',  ( 2.781799176224414971, -3.750297231070458537, -44.10000000002499121 ) ) ;
#17581=CARTESIAN_POINT ( 'NONE',  ( 5.925978784015399903, -0.8792241758803844842, -46.13818262062499542 ) ) ;
#17594=CARTESIAN_POINT ( 'NONE',  ( 1.592968524163114852, 5.205024221813498109, -52.26125421252498882 ) ) ;
#17632=( LENGTH_UNIT ( ) NAMED_UNIT ( * ) SI_UNIT ( .MILLI., .METRE. ) );
#17657=CARTESIAN_POINT ( 'NONE',  ( 0.9634065801723908917, -5.189854773623245876, -57.99125695792501034 ) ) ;
#17661=CARTESIAN_POINT ( 'NONE',  ( -4.439243896310288484, 1.104759232538872205, -68.10000000002500542 ) ) ;
#17670=CARTESIAN_POINT ( 'NONE',  ( -5.505147662677075004, -0.2930537998028365232, -64.76421022022501006 ) ) ;
#17704=CARTESIAN_POINT ( 'NONE',  ( 5.896017893897736784, 2.415859114112482775, -61.37141554682499134 ) ) ;
#17717=CARTESIAN_POINT ( 'NONE',  ( 1.728339646750869818, -3.757809983586919866, -44.10000000002499121 ) ) ;
#17722=AXIS2_PLACEMENT_3D ( 'NONE', #2627, #14015, #29203 ) ;
#17725=SURFACE_STYLE_USAGE ( .BOTH. , #8127 ) ;
#17727=CARTESIAN_POINT ( 'NONE',  ( -3.917812474729757799, -3.807994372373406211, -46.40083066912499277 ) ) ;
#17738=CARTESIAN_POINT ( 'NONE',  ( -3.745704904464692842, -4.048335345151853559, -50.99612412472499301 ) ) ;
#17811=CARTESIAN_POINT ( 'NONE',  ( 4.332295931058598448, 4.388630459628991787, -57.22805965152500107 ) ) ;
#17818=CARTESIAN_POINT ( 'NONE',  ( -4.225732272487059404, 0.7470832582109949715, -68.10000000002500542 ) ) ;
#17829=CARTESIAN_POINT ( 'NONE',  ( 0.8372177269581373427, 4.490875019823951320, -63.02744533512500169 ) ) ;
#17858=CARTESIAN_POINT ( 'NONE',  ( -0.8249440165340113928, 4.504533947698903695, -60.25324387862499975 ) ) ;
#17872=EDGE_LOOP ( 'NONE', ( #9393, #20270 ) ) ;
#17873=CARTESIAN_POINT ( 'NONE',  ( -2.098672137722010334, -3.287437779826620776, -44.10000000002499121 ) ) ;
#17882=CARTESIAN_POINT ( 'NONE',  ( -5.843148694310191793, 0.5835664591014033675, -46.82737393802500492 ) ) ;
#17894=CARTESIAN_POINT ( 'NONE',  ( 4.762123832160154890, 2.112064333128992555, -52.62998794302499306 ) ) ;
#17960=CARTESIAN_POINT ( 'NONE',  ( 4.332295931058598448, 4.388630459628991787, -57.70805965152499795 ) ) ;
#17980=CARTESIAN_POINT ( 'NONE',  ( -1.219854050253890598, 4.750520449216602437, -66.20876360982499875 ) ) ;
#18014=CARTESIAN_POINT ( 'NONE',  ( -5.941465883516308999, 0.03012783874251079297, -62.57122063482501062 ) ) ;
#18029=CARTESIAN_POINT ( 'NONE',  ( 0.1566502184896971517, -3.976918879132022688, -44.10000000002499121 ) ) ;
#18039=CARTESIAN_POINT ( 'NONE',  ( 4.421972129926212247, 1.961202595004083005, -51.87998794302499306 ) ) ;
#18052=CARTESIAN_POINT ( 'NONE',  ( -4.320323480314926634, -1.509945384023519965, -50.80743646232500765 ) ) ;
#18125=CARTESIAN_POINT ( 'NONE',  ( -2.948077164825098517, -3.495793300896359312, -58.77407541852498696 ) ) ;
#18143=CARTESIAN_POINT ( 'NONE',  ( 6.385918709370476343, 0.1527399656023400998, -64.06686508972499894 ) ) ;
#18162=CARTESIAN_POINT ( 'NONE',  ( -4.064488300603595228, -4.392874523441014034, -50.19612412472499585 ) ) ;
#18169=CARTESIAN_POINT ( 'NONE',  ( 2.795517707053192691, -3.729300093007118289, -68.10000000002500542 ) ) ;
#18176=CARTESIAN_POINT ( 'NONE',  ( -1.595193757947241497, 6.212219048941578059, -66.68876360962499916 ) ) ;
#18201=CARTESIAN_POINT ( 'NONE',  ( -4.652656055762370180, -1.626095028925849562, -49.65743646232498776 ) ) ;
#18211=CARTESIAN_POINT ( 'NONE',  ( -5.212126283948660621, -2.851000302232811201, -53.34982952342500084 ) ) ;
#18285=CARTESIAN_POINT ( 'NONE',  ( 5.896017893897736784, 2.415859114112482775, -60.89141554682500157 ) ) ;
#18308=CARTESIAN_POINT ( 'NONE',  ( -0.8291470764733243071, -4.443337602648614215, -67.50745670422500666 ) ) ;
#18329=CARTESIAN_POINT ( 'NONE',  ( -5.463799992266447525, -1.435916617982112342, -56.45102360502500005 ) ) ;
#18335=CARTESIAN_POINT ( 'NONE',  ( 2.572981240252346868, -3.481270928177104818, -68.10000000002499121 ) ) ;
#18339=CARTESIAN_POINT ( 'NONE',  ( -4.246103237644704542, 0.8932448209632969371, -44.10000000002499121 ) ) ;
#18344=CARTESIAN_POINT ( 'NONE',  ( -1.470080522021702363, 5.724986182348157371, -67.00876360962500655 ) ) ;
#18364=CARTESIAN_POINT ( 'NONE',  ( -0.1685424049532343038, -3.960684645455483377, -44.10000000002498410 ) ) ;
#18373=CARTESIAN_POINT ( 'NONE',  ( 1.321824945545745145, 4.319062652178982553, -51.46125421262499344 ) ) ;
#18381=CARTESIAN_POINT ( 'NONE',  ( -3.985743628842679076, -2.180176701716177057, -53.34982952342500084 ) ) ;
#18415=CARTESIAN_POINT ( 'NONE',  ( 0.5498575204214891654, -4.501552459773711767, -44.18057807742500387 ) ) ;
#18445=CARTESIAN_POINT ( 'NONE',  ( 1.672654430053971852, 5.259243695923226269, -59.66492395752499789 ) ) ;
#18463=CARTESIAN_POINT ( 'NONE',  ( 4.441146713721680683, -1.990734395214994734, -66.87841551502499726 ) ) ;
#18482=CARTESIAN_POINT ( 'NONE',  ( 5.235465350887244185, -2.882605534178610984, -58.30843849682499780 ) ) ;
#18491=CARTESIAN_POINT ( 'NONE',  ( 2.491610509676117857, -3.506118418580284946, -68.10000000002500542 ) ) ;
#18496=CARTESIAN_POINT ( 'NONE',  ( -4.411068591882468581, 1.131342447431700871, -44.10000000002499121 ) ) ;
#18500=CARTESIAN_POINT ( 'NONE',  ( 3.542472921321142110, 4.818407451951889797, -66.64226422552501106 ) ) ;
#18523=CARTESIAN_POINT ( 'NONE',  ( -0.9881560945370695404, 5.823346091562972227, -50.77792092402498980 ) ) ;
#18534=CARTESIAN_POINT ( 'NONE',  ( -1.065285671501096765, -5.119323817795550902, -53.67706695232500635 ) ) ;
#18551=CARTESIAN_POINT ( 'NONE',  ( -4.498618707852113374, 2.988074248075567318, -44.10000000002499121 ) ) ;
#18571=CARTESIAN_POINT ( 'NONE',  ( 2.472051776111518162, -3.869239954018615535, -44.31966640442499994 ) ) ;
#18602=CARTESIAN_POINT ( 'NONE',  ( 4.508719565894404369, 1.847421675581905953, -60.49141554682498878 ) ) ;
#18617=CARTESIAN_POINT ( 'NONE',  ( -1.084269253894827534, -5.810518403417324507, -67.42745670422499416 ) ) ;
#18636=CARTESIAN_POINT ( 'NONE',  ( 3.449241269337446791, -4.803451378176493591, -61.52197827312500067 ) ) ;
#18643=CARTESIAN_POINT ( 'NONE',  ( 2.400858303373162528, -3.536441939007071600, -68.10000000002501963 ) ) ;
#18645=CARTESIAN_POINT ( 'NONE',  ( -4.245077499289021894, 0.8871105264785797972, -44.10000000002499121 ) ) ;
#18649=CARTESIAN_POINT ( 'NONE',  ( 4.962532606735698515, 2.397722036449358107, -67.65315453642499222 ) ) ;
#18674=CARTESIAN_POINT ( 'NONE',  ( 0.6613659943793989138, -4.850238491497672833, -49.36468436622500633 ) ) ;
#18683=CARTESIAN_POINT ( 'NONE',  ( 3.357378826396555382, -2.722208303779470651, -55.80923804942499800 ) ) ;
#18689=PRODUCT_DEFINITION_SHAPE ( 'NONE', 'NONE',  #4652 ) ;
#18722=CARTESIAN_POINT ( 'NONE',  ( 4.248246898893026646, -2.821772188863608921, -43.35875473022499449 ) ) ;
#18755=CARTESIAN_POINT ( 'NONE',  ( 1.387947292976102087, 4.364053279572885025, -60.46492395752500215 ) ) ;
#18771=CARTESIAN_POINT ( 'NONE',  ( 4.782773383987898974, -2.143867810222768178, -66.52841551492500116 ) ) ;
#18798=CARTESIAN_POINT ( 'NONE',  ( 2.608536516501943403, -3.962017450064297286, -68.10000000002500542 ) ) ;
#18805=CARTESIAN_POINT ( 'NONE',  ( 2.917330641183085049, 3.968100254485465328, -67.39226422542500927 ) ) ;
#18834=CARTESIAN_POINT ( 'NONE',  ( -3.221934060409652023, 3.671197199744479001, -53.98587006832499924 ) ) ;
#18843=CARTESIAN_POINT ( 'NONE',  ( 4.046071919042645959, -3.280610007112897186, -56.20923804942499657 ) ) ;
#18871=CARTESIAN_POINT ( 'NONE',  ( -4.592700181227117540, -1.655560342997611123, -44.01497819512500342 ) ) ;
#18885=CARTESIAN_POINT ( 'NONE',  ( -4.757978549728680839, 2.797812790916673897, -45.64354844312499893 ) ) ;
#18929=CARTESIAN_POINT ( 'NONE',  ( 2.708949881112997282, 3.684664522020660193, -66.64226422532500749 ) ) ;
#18956=CARTESIAN_POINT ( 'NONE',  ( -4.781437088831645532, 0.4141712122942822205, -68.10000000002500542 ) ) ;
#18967=CARTESIAN_POINT ( 'NONE',  ( 0.8372177269581546621, 4.490875019823945991, -63.42744533512499316 ) ) ;
#18989=CARTESIAN_POINT ( 'NONE',  ( 6.136659917679837761, 0.6935318534637759935, -54.53771407622500078 ) ) ;
#18998=CARTESIAN_POINT ( 'NONE',  ( -4.178199994060139311, -1.098053884355550069, -56.85102360502499153 ) ) ;
#19026=CARTESIAN_POINT ( 'NONE',  ( -2.036891525988612894, -5.569677580567498509, -43.98640794712500224 ) ) ;
#19038=CARTESIAN_POINT ( 'NONE',  ( 4.248246898893026646, -2.821772188863608921, -43.83875473022499847 ) ) ;
#19122=CARTESIAN_POINT ( 'NONE',  ( -1.449312944839797890, 3.998683954144016894, -69.15099036452500059 ) ) ;
#19126=CARTESIAN_POINT ( 'NONE',  ( 3.389692407805913632, 3.523397910813151679, -48.69426496242499525 ) ) ;
#19158=CARTESIAN_POINT ( 'NONE',  ( -0.06606756225350368661, 5.646037861211643083, -57.31818518972499277 ) ) ;
#19182=CARTESIAN_POINT ( 'NONE',  ( 2.472051776111518162, -3.869239954018615535, -42.81966640442499994 ) ) ;
#19196=CARTESIAN_POINT ( 'NONE',  ( 4.531630834892029114, -0.6723478992683162847, -46.53818262062500111 ) ) ;
#19269=CARTESIAN_POINT ( 'NONE',  ( -1.864922697349092662, -4.767250968724650484, -68.10000000002503384 ) ) ;
#19285=CARTESIAN_POINT ( 'NONE',  ( 2.833778097863427714, 3.583098331959792660, -63.63768011632500787 ) ) ;
#19317=CARTESIAN_POINT ( 'NONE',  ( -5.545418199629476241, -2.237997381628727300, -59.86491726642499600 ) ) ;
#19356=CARTESIAN_POINT ( 'NONE',  ( 3.054834669310706907, -5.027794097514915350, -47.36669147672500202 ) ) ;
#19424=CARTESIAN_POINT ( 'NONE',  ( -4.862250760564064578, -0.002988278297125585882, -68.10000000002500542 ) ) ;
#19437=CARTESIAN_POINT ( 'NONE',  ( -3.250950776947245213, -3.159825117472807143, -47.20083066912499703 ) ) ;
#19470=CARTESIAN_POINT ( 'NONE',  ( 3.567773119718944397, 3.614166260817118559, -58.45805965152499084 ) ) ;
#19488=CARTESIAN_POINT ( 'NONE',  ( 1.408406170841865812, -4.736705221900152196, -44.10000000002499831 ) ) ;
#19511=CARTESIAN_POINT ( 'NONE',  ( 5.925978784015399903, -0.8792241758803844842, -46.13818262062499542 ) ) ;
#19551=CARTESIAN_POINT ( 'NONE',  ( -3.229037295491567150, -3.989637411031741632, -44.10000000002499121 ) ) ;
#19579=CARTESIAN_POINT ( 'NONE',  ( -1.293561172433232986, -6.216321778783836294, -52.92706695232499925 ) ) ;
#19590=CARTESIAN_POINT ( 'NONE',  ( -3.447099378712505935, 3.428612291819206792, -69.69322600202499984 ) ) ;
#19596=CARTESIAN_POINT ( 'NONE',  ( -4.150389416700803302, 1.923785201099231790, -65.77526299422500244 ) ) ;
#19623=CARTESIAN_POINT ( 'NONE',  ( -2.158984558600606007, 5.217364672555318883, -57.62652090042499964 ) ) ;
#19639=CARTESIAN_POINT ( 'NONE',  ( 1.764726261278249497, -3.747269161217322786, -44.10000000002499831 ) ) ;
#19650=CARTESIAN_POINT ( 'NONE',  ( -1.460566089872937789, -4.291843709425559261, -46.59520033292501040 ) ) ;
#19662=CARTESIAN_POINT ( 'NONE',  ( -0.5163256777700186984, 4.538631023554793309, -48.66410749632500199 ) ) ;
#19703=CARTESIAN_POINT ( 'NONE',  ( -4.469433717901757142, 1.081650411600142414, -44.10000000002499831 ) ) ;
#19707=( NAMED_UNIT ( * ) SI_UNIT ( $, .STERADIAN. ) SOLID_ANGLE_UNIT ( ) );
#19734=CARTESIAN_POINT ( 'NONE',  ( -4.890954027197769172, -0.1236851485019374169, -52.80673954922500712 ) ) ;
#19739=CARTESIAN_POINT ( 'NONE',  ( -4.773704105810320897, 0.4428995197802990669, -68.10000000002500542 ) ) ;
#19780=CARTESIAN_POINT ( 'NONE',  ( -4.880917369133354278, -2.481566535878938495, -63.16424626872499459 ) ) ;
#19798=CARTESIAN_POINT ( 'NONE',  ( 2.710954907126704061, -3.448654721267146783, -44.10000000002499831 ) ) ;
#19804=CARTESIAN_POINT ( 'NONE',  ( 4.531630834892029114, -0.6723478992683162847, -45.73818262062500395 ) ) ;
#19806=SHAPE_REPRESENTATION ( 'Catch Spring', ( #17722 ), #23393 ) ;
#19821=CARTESIAN_POINT ( 'NONE',  ( -3.250950776947245213, -3.159825117472807143, -47.20083066912499703 ) ) ;
#19892=CARTESIAN_POINT ( 'NONE',  ( -1.650988191866312516, 3.989749455477759721, -56.74652090042498997 ) ) ;
#19895=CARTESIAN_POINT ( 'NONE',  ( -4.269058662706476603, 1.003599612145581021, -68.10000000002500542 ) ) ;
#19903=CARTESIAN_POINT ( 'NONE',  ( 1.094823181362614140, 5.872682718251108547, -63.42744533522500205 ) ) ;
#19905=CARTESIAN_POINT ( 'NONE',  ( 0.4446548587409490660, -4.237356817840251644, -67.77495035202500162 ) ) ;
#19931=CARTESIAN_POINT ( 'NONE',  ( 1.494712469390715892, 4.699749685697345747, -61.21492395752499505 ) ) ;
#19945=CARTESIAN_POINT ( 'NONE',  ( 2.852669508774048790, -3.465077913054150471, -44.10000000002499121 ) ) ;
#19954=CARTESIAN_POINT ( 'NONE',  ( 3.314820598666778917, -5.455691467570147779, -46.08669147682499556 ) ) ;
#19965=CARTESIAN_POINT ( 'NONE',  ( -0.9106536557335528359, 5.366613064751446949, -52.05792092402499804 ) ) ;
#20035=CARTESIAN_POINT ( 'NONE',  ( -4.072259770650454413, 2.021700601781299511, -56.79877225282499609 ) ) ;
#20041=CARTESIAN_POINT ( 'NONE',  ( -4.241725247297924994, 0.8684248349431030745, -68.10000000002500542 ) ) ;
#20052=CARTESIAN_POINT ( 'NONE',  ( 3.705709820302785396, 4.685590126413917034, -63.63768011632500787 ) ) ;
#20056=CARTESIAN_POINT ( 'NONE',  ( 2.708949881112997282, 3.684664522020660193, -66.64226422532500749 ) ) ;
#20087=CARTESIAN_POINT ( 'NONE',  ( 6.379024725906915272, -4.237078256518207908, -68.10000000002500542 ) ) ;
#20090=CARTESIAN_POINT ( 'NONE',  ( -4.361670840543652616, -2.217570095850531775, -63.11424626872499744 ) ) ;
#20107=CARTESIAN_POINT ( 'NONE',  ( 2.012151113573330985, -3.669704564848118800, -44.10000000002499831 ) ) ;
#20114=CARTESIAN_POINT ( 'NONE',  ( -2.393684743089937061, 3.904820337558664978, -45.05531229042499319 ) ) ;
#20126=CARTESIAN_POINT ( 'NONE',  ( -3.108138112192390778, -3.359256988581870385, -50.19612412472499585 ) ) ;
#20186=CARTESIAN_POINT ( 'NONE',  ( -1.256295066205788347, -5.815478746186413694, -55.93033560642499680 ) ) ;
#20191=CARTESIAN_POINT ( 'NONE',  ( -4.770183054246150967, 0.4556413907088688875, -68.10000000002500542 ) ) ;
#20201=CARTESIAN_POINT ( 'NONE',  ( 1.082264403401735020, -4.420062499635217357, -64.70397119102501904 ) ) ;
#20232=CARTESIAN_POINT ( 'NONE',  ( -4.300317018729668206, 2.364939115720630980, -59.81908057272499946 ) ) ;
#20245=CARTESIAN_POINT ( 'NONE',  ( 1.952025570637784035, -4.468452838841612262, -44.10000000002499831 ) ) ;
#20255=CARTESIAN_POINT ( 'NONE',  ( -3.250950776947245213, -3.159825117472807143, -47.20083066912499703 ) ) ;
#20268=CARTESIAN_POINT ( 'NONE',  ( 4.421972129926212247, 1.961202595004083005, -51.87998794302499306 ) ) ;
#20270=ORIENTED_EDGE ( 'NONE', *, *, #1514, .T. ) ;
#20340=CARTESIAN_POINT ( 'NONE',  ( -4.180007949804073419, -3.103635835586971758, -55.47895058492500198 ) ) ;
#20347=CARTESIAN_POINT ( 'NONE',  ( -4.229156943520672840, 0.7760457000830683905, -68.10000000002500542 ) ) ;
#20359=CARTESIAN_POINT ( 'NONE',  ( 1.082264403396195673, -4.420062499643547582, -64.30397119102499914 ) ) ;
#20378=CARTESIAN_POINT ( 'NONE',  ( -2.744417411265728912, -4.298957096598221561, -44.10000000002499121 ) ) ;
#20387=CARTESIAN_POINT ( 'NONE',  ( 0.8240483502834883289, -3.944499275425427776, -68.10000000002501963 ) ) ;
#20389=CARTESIAN_POINT ( 'NONE',  ( -3.607711123481817328, -1.653375552380872637, -44.10000000002498410 ) ) ;
#20394=CARTESIAN_POINT ( 'NONE',  ( -1.143212971672624478, -4.711439499498765393, -62.34311227092499053 ) ) ;
#20415=CARTESIAN_POINT ( 'NONE',  ( -0.8137756071791968360, 4.795696781221863603, -50.50792092402500799 ) ) ;
#20426=CARTESIAN_POINT ( 'NONE',  ( 4.101176313917073379, -1.931410228222276038, -52.69872167392500018 ) ) ;
#20496=CARTESIAN_POINT ( 'NONE',  ( 4.921121033118705412, -0.08698047164986451307, -57.34793411332498891 ) ) ;
#20503=CARTESIAN_POINT ( 'NONE',  ( -4.005572406160169407, -0.6430491863098631855, -68.10000000002503384 ) ) ;
#20515=CARTESIAN_POINT ( 'NONE',  ( -3.807105672867752588, -5.136256491769870536, -64.65409070562499494 ) ) ;
#20541=CARTESIAN_POINT ( 'NONE',  ( 2.746262074154482313, -3.444807799140186422, -68.10000000002501963 ) ) ;
#20548=CARTESIAN_POINT ( 'NONE',  ( 4.117846205589238195, 1.989599136607399954, -67.25315453642500074 ) ) ;
#20573=CARTESIAN_POINT ( 'NONE',  ( -0.9881560945370695404, 5.823346091562972227, -51.25792092402499378 ) ) ;
#20584=CARTESIAN_POINT ( 'NONE',  ( -4.535753307212162078, -3.367775055652930227, -56.75895058492499601 ) ) ;
#20657=CARTESIAN_POINT ( 'NONE',  ( 4.855544147916073250, 1.989531035200713838, -60.14141554682500868 ) ) ;
#20676=CARTESIAN_POINT ( 'NONE',  ( 2.917330641183085049, 3.968100254485465328, -65.89226422532500749 ) ) ;
#20693=CARTESIAN_POINT ( 'NONE',  ( 2.743362564037614248, -4.941860934411918649, -55.58172062782499268 ) ) ;
#20700=CARTESIAN_POINT ( 'NONE',  ( 2.412358317651485784, -3.532528282628375926, -68.10000000002500542 ) ) ;
#20704=CARTESIAN_POINT ( 'NONE',  ( -4.258588862633405192, 0.9647698903526967795, -44.10000000002498410 ) ) ;
#20708=CARTESIAN_POINT ( 'NONE',  ( -1.595193757947241497, 6.212219048941578059, -66.20876360962500939 ) ) ;
#20734=CARTESIAN_POINT ( 'NONE',  ( 4.085013927406620837, 4.246146200131522441, -47.89426496242500519 ) ) ;
#20744=CARTESIAN_POINT ( 'NONE',  ( 0.7192951553254764985, 4.518739695583327887, -54.41500058692499664 ) ) ;
#20757=PLANE ( 'NONE',  #7461 ) ;
#20814=CARTESIAN_POINT ( 'NONE',  ( -1.143212971672624478, -4.711439499498765393, -61.54311227092500758 ) ) ;
#20822=CARTESIAN_POINT ( 'NONE',  ( -2.486632795208609803, -3.039739661661432280, -68.10000000002499121 ) ) ;
#20835=CARTESIAN_POINT ( 'NONE',  ( -3.447099378712505935, 3.428612291819206792, -68.19322600342499641 ) ) ;
#20860=CARTESIAN_POINT ( 'NONE',  ( 3.599561039400463347, 4.779710538180673041, -54.62619010302499589 ) ) ;
#20866=CARTESIAN_POINT ( 'NONE',  ( 1.172141357840190468, -3.890077810869508657, -68.10000000002501963 ) ) ;
#20869=CARTESIAN_POINT ( 'NONE',  ( -4.332055453559614300, 1.117314083138565284, -44.10000000002499121 ) ) ;
#20874=CARTESIAN_POINT ( 'NONE',  ( 4.117846205589234643, 1.989599136607407504, -66.85315453642499506 ) ) ;
#20899=CARTESIAN_POINT ( 'NONE',  ( 1.728540313474559387, 5.648005006634932990, -51.46125421262499344 ) ) ;
#20907=CARTESIAN_POINT ( 'NONE',  ( -0.9891938378274525157, -4.753657830815115837, -52.92706695232499925 ) ) ;
#20955=EDGE_LOOP ( 'NONE', ( #8774, #11628, #24008, #30434 ) ) ;
#20968=CARTESIAN_POINT ( 'NONE',  ( 4.009291712408949770, -2.091746824018178685, -61.31790713612500099 ) ) ;
#20988=CARTESIAN_POINT ( 'NONE',  ( 5.807653394784360934, -2.603268055249425394, -66.79841551502499897 ) ) ;
#21010=CARTESIAN_POINT ( 'NONE',  ( -1.909971040720825908, -5.612411004515823088, -46.99520033292500187 ) ) ;
#21017=CARTESIAN_POINT ( 'NONE',  ( 2.729399839092999436, -3.446420600438925508, -68.10000000002500542 ) ) ;
#21021=CARTESIAN_POINT ( 'NONE',  ( -4.201749689532753962, 0.5185635314718879396, -44.10000000002499831 ) ) ;
#21025=CARTESIAN_POINT ( 'NONE',  ( -3.807105672873282831, -5.136256491778199873, -65.13409070562501313 ) ) ;
#21051=CARTESIAN_POINT ( 'NONE',  ( 1.592968524163114852, 5.205024221813498109, -50.66125421252500161 ) ) ;
#21064=CARTESIAN_POINT ( 'NONE',  ( 4.390418465362644795, -3.559810858784186127, -55.40923804942499942 ) ) ;
#21099=CARTESIAN_POINT ( 'NONE',  ( -4.592700181227121980, -1.655560342997616896, -44.41497819512500200 ) ) ;
#21129=CARTESIAN_POINT ( 'NONE',  ( -1.078772944755383767, 5.890544393200768170, -60.25324387862499975 ) ) ;
#21144=CARTESIAN_POINT ( 'NONE',  ( 3.542472921321142110, 4.818407451951889797, -66.16226422552499287 ) ) ;
#21168=CARTESIAN_POINT ( 'NONE',  ( 2.713364190111911434, -3.841189043361406430, -68.10000000002503384 ) ) ;
#21176=CARTESIAN_POINT ( 'NONE',  ( -5.427432314178970429, 2.515719109140460041, -66.25526299442500999 ) ) ;
#21201=CARTESIAN_POINT ( 'NONE',  ( 2.528196872781957705, -4.554263998399506796, -54.78172062782500973 ) ) ;
#21208=CARTESIAN_POINT ( 'NONE',  ( 0.9406167415608388538, 5.909121140422558760, -54.41500058692499664 ) ) ;
#21218=MANIFOLD_SOLID_BREP ( 'PartBody', #1506 ) ;
#21236=CARTESIAN_POINT ( 'NONE',  ( 4.248246898893026646, -2.821772188863608921, -42.87875473022499762 ) ) ;
#21249=CARTESIAN_POINT ( 'NONE',  ( 0.6626488065253229864, -5.424947836095445730, -44.58057807742500955 ) ) ;
#21278=CARTESIAN_POINT ( 'NONE',  ( -5.545418199629476241, -2.237997381628727300, -59.38491726642499202 ) ) ;
#21296=CARTESIAN_POINT ( 'NONE',  ( 1.515105966928380399, -5.232275150219822812, -66.90367649362498526 ) ) ;
#21324=CARTESIAN_POINT ( 'NONE',  ( 0.9411048234942640534, -4.889285007102426306, -68.10000000002503384 ) ) ;
#21328=CARTESIAN_POINT ( 'NONE',  ( -4.846949687726242573, -1.117598880638678738, -44.10000000002499121 ) ) ;
#21332=CARTESIAN_POINT ( 'NONE',  ( -4.185763533044374540, 4.163314928055855901, -68.94322600512501253 ) ) ;
#21361=CARTESIAN_POINT ( 'NONE',  ( 4.390418465360985678, -3.559810858786684129, -54.92923804942499544 ) ) ;
#21370=B_SPLINE_CURVE_WITH_KNOTS ( 'NONE', 5,
 ( #30778, #23085, #6851, #6391, #9532, #9996, #29175, #2909, #2455, #7169, #7015, #9841, #19437, #4818, #21801, #5111, #19126, #258, #12501, #5269, #14882, #28573, #29027, #16910, #23860, #14414, #24473, #100, #24310, #16757, #21652, #26520, #28876, #4960, #12188, #2761, #26824, #17071, #7476, #7327, #30937, #9362, #21491, #12047, #4648, #14573, #28722, #26669, #11887, #7624, #2305, #16605, #26373, #24014, #17219, #14719, #9681, #413, #31089, #18967, #19285, #24160, #12354, #21961, #14259, #2601, #19596, #26213, #20056, #17530, #7776, #15484, #19905, #15030, #15333 ),
 .UNSPECIFIED., .F., .F.,
 ( 6, 3, 3, 3, 3, 3, 3, 3, 3, 3, 3, 3, 3, 3, 3, 3, 3, 3, 3, 3, 3, 3, 3, 3, 6 ),
 ( 8.127326494049999184, 11.49596029219999949, 23.35952330949999833, 35.23214498380000492, 46.71570041139999319, 58.48118637179999268, 70.16173614769999745, 81.99711437660000968, 93.33986353700001359, 104.8204913790000035, 116.3828353250000021, 128.2105526469999859, 137.7231253239999944, 147.2120576640000138, 156.6774103699999898, 168.4624398839999913, 180.2684855139999911, 192.1268167670000082, 203.5147100690000173, 215.0810220189999882, 226.8492753339999979, 238.4740513719999910, 250.2932425120000062, 262.1023078380000015, 271.0195818650000206 ),
 .UNSPECIFIED. ) ;
#21371=CARTESIAN_POINT ( 'NONE',  ( -4.240613917342964889, -1.711409762446096439, -59.78491726642500481 ) ) ;
#21373=( BOUNDED_SURFACE ( )  B_SPLINE_SURFACE ( 5, 5, ( 
 ( #18722, #19038, #15904, #6610, #30388, #3947 ),
 ( #1901, #13540, #2057, #18571, #23152, #16059 ),
 ( #23304, #4566, #21249, #30849, #18415, #1594 ),
 ( #11182, #9280, #16520, #4414, #13700, #25825 ),
 ( #28171, #4260, #13859, #23467, #11496, #21099 ),
 ( #25976, #30694, #18885, #16366, #28324, #6770 ),
 ( #28480, #6921, #26130, #14170, #21715, #636 ),
 ( #483, #24081, #28947, #24226, #5029, #2668 ),
 ( #16985, #4724, #12106, #29096, #14637, #22175 ),
 ( #19511, #17134, #14483, #17292, #19196, #9749 ),
 ( #165, #14, #19356, #24388, #7388, #2823 ),
 ( #26589, #7685, #9597, #10218, #2521, #28781 ),
 ( #12264, #21882, #16671, #14940, #327, #19821 ),
 ( #7081, #9908, #7543, #26736, #26899, #7238 ),
 ( #5173, #26280, #14335, #5336, #14787, #12415 ),
 ( #22032, #16831, #23933, #2370, #19662, #10065 ),
 ( #29246, #24540, #2979, #26438, #4878, #11956 ),
 ( #12569, #21565, #12883, #27500, #5947, #29715 ),
 ( #27050, #13179, #3584, #8142, #29404, #27355 ),
 ( #8455, #24849, #6100, #3278, #22332, #7995 ),
 ( #22487, #15545, #17738, #10674, #10994, #20126 ),
 ( #5798, #1397, #3430, #25152, #18052, #3755 ),
 ( #10375, #936, #13030, #22792, #29560, #1243 ),
 ( #5487, #10528, #19965, #3123, #15395, #24994 ),
 ( #10841, #22639, #17594, #27658, #15697, #13347 ),
 ( #15094, #27202, #8299, #17894, #1082, #20268 ),
 ( #5641, #29866, #7839, #15238, #20426, #30021 ),
 ( #25311, #22952, #784, #17442, #24688, #12722 ),
 ( #6421, #11307, #6573, #18534, #16173, #20907 ),
 ( #18211, #25636, #11461, #28135, #4530, #18381 ),
 ( #30662, #27979, #30809, #1558, #23267, #25786 ),
 ( #23119, #6268, #30345, #4066, #6876, #1861 ),
 ( #21208, #11147, #14133, #16020, #13502, #20744 ),
 ( #25473, #4218, #13661, #1707, #13820, #30506 ),
 ( #13977, #8935, #8775, #23434, #23738, #30181 ),
 ( #21064, #6726, #18843, #9087, #18683, #2174 ),
 ( #16331, #9236, #26094, #28285, #25938, #4373 ),
 ( #23588, #2025, #11612, #28445, #27817, #16480 ),
 ( #3907, #20584, #8611, #15871, #24346, #4992 ),
 ( #21990, #10028, #26858, #23897, #18998, #21522 ),
 ( #21835, #16788, #2632, #17100, #29924, #12224 ),
 ( #9560, #19623, #28746, #28605, #9870, #11766 ),
 ( #19158, #293, #9396, #17248, #26551, #26247 ),
 ( #26698, #2334, #24042, #19470, #14749, #16944 ),
 ( #29061, #29205, #24500, #5303, #14290, #447 ),
 ( #7199, #7506, #11917, #7650, #26403, #7043 ),
 ( #4845, #14906, #24190, #14445, #12382, #2486 ),
 ( #30965, #12073, #5137, #2789, #16633, #9710 ),
 ( #21681, #19317, #131, #4683, #21371, #28909 ),
 ( #14602, #7355, #12532, #12849, #24960, #20232 ),
 ( #3391, #10640, #3241, #1047, #596, #17858 ),
 ( #5758, #5602, #10338, #19931, #29981, #3086 ),
 ( #15664, #17704, #15363, #22451, #17559, #29826 ),
 ( #12996, #2939, #24806, #22608, #8415, #12683 ),
 ( #22139, #27318, #8264, #899, #27167, #27465 ),
 ( #5907, #10181, #10492, #15509, #20394, #27621 ),
 ( #7806, #6067, #19780, #20090, #29363, #25116 ),
 ( #18014, #22293, #3551, #29520, #22754, #13144 ),
 ( #17405, #27011, #1203, #5452, #10799, #15058 ),
 ( #24653, #29681, #747, #7958, #8108, #15204 ),
 ( #13626, #27945, #11268, #4183, #30145, #13780 ),
 ( #13462, #1990, #11112, #1360, #23399, #25273 ),
 ( #3872, #1830, #22919, #30773, #8896, #8575 ),
 ( #30627, #15834, #6387, #11424, #28248, #30471 ),
 ( #21025, #11579, #6848, #9202, #27780, #13941 ),
 ( #23078, #9054, #6225, #23552, #25440, #10953 ),
 ( #30306, #21176, #6539, #8737, #25908, #1521 ),
 ( #20708, #18176, #18344, #15984, #25595, #3708 ),
 ( #18500, #28413, #6693, #18805, #4028, #28098 ),
 ( #13308, #23230, #18649, #1672, #20548, #20874 ),
 ( #16136, #25751, #16293, #4343, #26209, #4499 ),
 ( #16751, #16449, #14409, #14566, #26664, #11884 ),
 ( #26368, #29171, #21796, #408, #9835, #24010 ),
 ( #21647, #2597, #5106, #21954, #9358, #28569 ),
 ( #2755, #16599, #12184, #23856, #14715, #251 ),
 ( #21332, #9991, #9675, #19590, #24156, #17065 ),
 ( #14099, #4814, #7469, #21488, #2450, #19122 ),
 ( #12041, #28716, #96, #26514, #30934, #4955 ) ),
 .UNSPECIFIED., .F., .F., .T. ) 
 B_SPLINE_SURFACE_WITH_KNOTS ( ( 6, 3, 3, 3, 3, 3, 3, 3, 3, 3, 3, 3, 3, 3, 3, 3, 3, 3, 3, 3, 3, 3, 3, 3, 3, 6 ),
 ( 6, 6 ),
 ( 0.000000000000000000, 11.49596029219999949, 23.35952330949999833, 35.23214498380000492, 46.71570041140000029, 58.48118637179999979, 70.16173614769999745, 81.99711437660000968, 93.33986353700001359, 104.8204913790000035, 116.3828353250000021, 128.2105526469999859, 137.7231253239999944, 147.2120576640000138, 156.6774103699999898, 168.4624398839999913, 180.2684855139999911, 192.1268167670000082, 203.5147100690000173, 215.0810220189999882, 226.8492753339999979, 238.4740513719999910, 250.2932425120000062, 262.1023078380000015, 273.4723917590000042, 284.7968047250000154 ),
 ( 6.674405137519999975, 13.34881027499999995 ),
 .UNSPECIFIED. ) 
 GEOMETRIC_REPRESENTATION_ITEM ( )  RATIONAL_B_SPLINE_SURFACE ( (
 ( 0.2500000000000000000, 0.2500000000000000000, 0.2999999999999999889, 0.4000000000000000222, 0.5999999999999999778, 1.000000000000000000),
 ( 0.2500000000000000000, 0.2500000000000000000, 0.2999999999999999889, 0.4000000000000000222, 0.5999999999999999778, 1.000000000000000000),
 ( 0.2500000000000000000, 0.2500000000000000000, 0.2999999999999999889, 0.4000000000000000222, 0.5999999999999999778, 1.000000000000000000),
 ( 0.2500000000000000000, 0.2500000000000000000, 0.2999999999999999889, 0.4000000000000000222, 0.5999999999999999778, 1.000000000000000000),
 ( 0.2500000000000000000, 0.2500000000000000000, 0.2999999999999999889, 0.4000000000000000222, 0.5999999999999999778, 1.000000000000000000),
 ( 0.2500000000000000000, 0.2500000000000000000, 0.2999999999999999889, 0.4000000000000000222, 0.5999999999999999778, 1.000000000000000000),
 ( 0.2500000000000000000, 0.2500000000000000000, 0.2999999999999999889, 0.4000000000000000222, 0.5999999999999999778, 1.000000000000000000),
 ( 0.2500000000000000000, 0.2500000000000000000, 0.2999999999999999889, 0.4000000000000000222, 0.5999999999999999778, 1.000000000000000000),
 ( 0.2500000000000000000, 0.2500000000000000000, 0.2999999999999999889, 0.4000000000000000222, 0.5999999999999999778, 1.000000000000000000),
 ( 0.2500000000000000000, 0.2500000000000000000, 0.2999999999999999889, 0.4000000000000000222, 0.5999999999999999778, 1.000000000000000000),
 ( 0.2500000000000000000, 0.2500000000000000000, 0.2999999999999999889, 0.4000000000000000222, 0.5999999999999999778, 1.000000000000000000),
 ( 0.2500000000000000000, 0.2500000000000000000, 0.2999999999999999889, 0.4000000000000000222, 0.5999999999999999778, 1.000000000000000000),
 ( 0.2500000000000000000, 0.2500000000000000000, 0.2999999999999999889, 0.4000000000000000222, 0.5999999999999999778, 1.000000000000000000),
 ( 0.2500000000000000000, 0.2500000000000000000, 0.2999999999999999889, 0.4000000000000000222, 0.5999999999999999778, 1.000000000000000000),
 ( 0.2500000000000000000, 0.2500000000000000000, 0.2999999999999999889, 0.4000000000000000222, 0.5999999999999999778, 1.000000000000000000),
 ( 0.2500000000000000000, 0.2500000000000000000, 0.2999999999999999889, 0.4000000000000000222, 0.5999999999999999778, 1.000000000000000000),
 ( 0.2500000000000000000, 0.2500000000000000000, 0.2999999999999999889, 0.4000000000000000222, 0.5999999999999999778, 1.000000000000000000),
 ( 0.2500000000000000000, 0.2500000000000000000, 0.2999999999999999889, 0.4000000000000000222, 0.5999999999999999778, 1.000000000000000000),
 ( 0.2500000000000000000, 0.2500000000000000000, 0.2999999999999999889, 0.4000000000000000222, 0.5999999999999999778, 1.000000000000000000),
 ( 0.2500000000000000000, 0.2500000000000000000, 0.2999999999999999889, 0.4000000000000000222, 0.5999999999999999778, 1.000000000000000000),
 ( 0.2500000000000000000, 0.2500000000000000000, 0.2999999999999999889, 0.4000000000000000222, 0.5999999999999999778, 1.000000000000000000),
 ( 0.2500000000000000000, 0.2500000000000000000, 0.2999999999999999889, 0.4000000000000000222, 0.5999999999999999778, 1.000000000000000000),
 ( 0.2500000000000000000, 0.2500000000000000000, 0.2999999999999999889, 0.4000000000000000222, 0.5999999999999999778, 1.000000000000000000),
 ( 0.2500000000000000000, 0.2500000000000000000, 0.2999999999999999889, 0.4000000000000000222, 0.5999999999999999778, 1.000000000000000000),
 ( 0.2500000000000000000, 0.2500000000000000000, 0.2999999999999999889, 0.4000000000000000222, 0.5999999999999999778, 1.000000000000000000),
 ( 0.2500000000000000000, 0.2500000000000000000, 0.2999999999999999889, 0.4000000000000000222, 0.5999999999999999778, 1.000000000000000000),
 ( 0.2500000000000000000, 0.2500000000000000000, 0.2999999999999999889, 0.4000000000000000222, 0.5999999999999999778, 1.000000000000000000),
 ( 0.2500000000000000000, 0.2500000000000000000, 0.2999999999999999889, 0.4000000000000000222, 0.5999999999999999778, 1.000000000000000000),
 ( 0.2500000000000000000, 0.2500000000000000000, 0.2999999999999999889, 0.4000000000000000222, 0.5999999999999999778, 1.000000000000000000),
 ( 0.2500000000000000000, 0.2500000000000000000, 0.2999999999999999889, 0.4000000000000000222, 0.5999999999999999778, 1.000000000000000000),
 ( 0.2500000000000000000, 0.2500000000000000000, 0.2999999999999999889, 0.4000000000000000222, 0.5999999999999999778, 1.000000000000000000),
 ( 0.2500000000000000000, 0.2500000000000000000, 0.2999999999999999889, 0.4000000000000000222, 0.5999999999999999778, 1.000000000000000000),
 ( 0.2500000000000000000, 0.2500000000000000000, 0.2999999999999999889, 0.4000000000000000222, 0.5999999999999999778, 1.000000000000000000),
 ( 0.2500000000000000000, 0.2500000000000000000, 0.2999999999999999889, 0.4000000000000000222, 0.5999999999999999778, 1.000000000000000000),
 ( 0.2500000000000000000, 0.2500000000000000000, 0.2999999999999999889, 0.4000000000000000222, 0.5999999999999999778, 1.000000000000000000),
 ( 0.2500000000000000000, 0.2500000000000000000, 0.2999999999999999889, 0.4000000000000000222, 0.5999999999999999778, 1.000000000000000000),
 ( 0.2500000000000000000, 0.2500000000000000000, 0.2999999999999999889, 0.4000000000000000222, 0.5999999999999999778, 1.000000000000000000),
 ( 0.2500000000000000000, 0.2500000000000000000, 0.2999999999999999889, 0.4000000000000000222, 0.5999999999999999778, 1.000000000000000000),
 ( 0.2500000000000000000, 0.2500000000000000000, 0.2999999999999999889, 0.4000000000000000222, 0.5999999999999999778, 1.000000000000000000),
 ( 0.2500000000000000000, 0.2500000000000000000, 0.2999999999999999889, 0.4000000000000000222, 0.5999999999999999778, 1.000000000000000000),
 ( 0.2500000000000000000, 0.2500000000000000000, 0.2999999999999999889, 0.4000000000000000222, 0.5999999999999999778, 1.000000000000000000),
 ( 0.2500000000000000000, 0.2500000000000000000, 0.2999999999999999889, 0.4000000000000000222, 0.5999999999999999778, 1.000000000000000000),
 ( 0.2500000000000000000, 0.2500000000000000000, 0.2999999999999999889, 0.4000000000000000222, 0.5999999999999999778, 1.000000000000000000),
 ( 0.2500000000000000000, 0.2500000000000000000, 0.2999999999999999889, 0.4000000000000000222, 0.5999999999999999778, 1.000000000000000000),
 ( 0.2500000000000000000, 0.2500000000000000000, 0.2999999999999999889, 0.4000000000000000222, 0.5999999999999999778, 1.000000000000000000),
 ( 0.2500000000000000000, 0.2500000000000000000, 0.2999999999999999889, 0.4000000000000000222, 0.5999999999999999778, 1.000000000000000000),
 ( 0.2500000000000000000, 0.2500000000000000000, 0.2999999999999999889, 0.4000000000000000222, 0.5999999999999999778, 1.000000000000000000),
 ( 0.2500000000000000000, 0.2500000000000000000, 0.2999999999999999889, 0.4000000000000000222, 0.5999999999999999778, 1.000000000000000000),
 ( 0.2500000000000000000, 0.2500000000000000000, 0.2999999999999999889, 0.4000000000000000222, 0.5999999999999999778, 1.000000000000000000),
 ( 0.2500000000000000000, 0.2500000000000000000, 0.2999999999999999889, 0.4000000000000000222, 0.5999999999999999778, 1.000000000000000000),
 ( 0.2500000000000000000, 0.2500000000000000000, 0.2999999999999999889, 0.4000000000000000222, 0.5999999999999999778, 1.000000000000000000),
 ( 0.2500000000000000000, 0.2500000000000000000, 0.2999999999999999889, 0.4000000000000000222, 0.5999999999999999778, 1.000000000000000000),
 ( 0.2500000000000000000, 0.2500000000000000000, 0.2999999999999999889, 0.4000000000000000222, 0.5999999999999999778, 1.000000000000000000),
 ( 0.2500000000000000000, 0.2500000000000000000, 0.2999999999999999889, 0.4000000000000000222, 0.5999999999999999778, 1.000000000000000000),
 ( 0.2500000000000000000, 0.2500000000000000000, 0.2999999999999999889, 0.4000000000000000222, 0.5999999999999999778, 1.000000000000000000),
 ( 0.2500000000000000000, 0.2500000000000000000, 0.2999999999999999889, 0.4000000000000000222, 0.5999999999999999778, 1.000000000000000000),
 ( 0.2500000000000000000, 0.2500000000000000000, 0.2999999999999999889, 0.4000000000000000222, 0.5999999999999999778, 1.000000000000000000),
 ( 0.2500000000000000000, 0.2500000000000000000, 0.2999999999999999889, 0.4000000000000000222, 0.5999999999999999778, 1.000000000000000000),
 ( 0.2500000000000000000, 0.2500000000000000000, 0.2999999999999999889, 0.4000000000000000222, 0.5999999999999999778, 1.000000000000000000),
 ( 0.2500000000000000000, 0.2500000000000000000, 0.2999999999999999889, 0.4000000000000000222, 0.5999999999999999778, 1.000000000000000000),
 ( 0.2500000000000000000, 0.2500000000000000000, 0.2999999999999999889, 0.4000000000000000222, 0.5999999999999999778, 1.000000000000000000),
 ( 0.2500000000000000000, 0.2500000000000000000, 0.2999999999999999889, 0.4000000000000000222, 0.5999999999999999778, 1.000000000000000000),
 ( 0.2500000000000000000, 0.2500000000000000000, 0.2999999999999999889, 0.4000000000000000222, 0.5999999999999999778, 1.000000000000000000),
 ( 0.2500000000000000000, 0.2500000000000000000, 0.2999999999999999889, 0.4000000000000000222, 0.5999999999999999778, 1.000000000000000000),
 ( 0.2500000000000000000, 0.2500000000000000000, 0.2999999999999999889, 0.4000000000000000222, 0.5999999999999999778, 1.000000000000000000),
 ( 0.2500000000000000000, 0.2500000000000000000, 0.2999999999999999889, 0.4000000000000000222, 0.5999999999999999778, 1.000000000000000000),
 ( 0.2500000000000000000, 0.2500000000000000000, 0.2999999999999999889, 0.4000000000000000222, 0.5999999999999999778, 1.000000000000000000),
 ( 0.2500000000000000000, 0.2500000000000000000, 0.2999999999999999889, 0.4000000000000000222, 0.5999999999999999778, 1.000000000000000000),
 ( 0.2500000000000000000, 0.2500000000000000000, 0.2999999999999999889, 0.4000000000000000222, 0.5999999999999999778, 1.000000000000000000),
 ( 0.2500000000000000000, 0.2500000000000000000, 0.2999999999999999889, 0.4000000000000000222, 0.5999999999999999778, 1.000000000000000000),
 ( 0.2500000000000000000, 0.2500000000000000000, 0.2999999999999999889, 0.4000000000000000222, 0.5999999999999999778, 1.000000000000000000),
 ( 0.2500000000000000000, 0.2500000000000000000, 0.2999999999999999889, 0.4000000000000000222, 0.5999999999999999778, 1.000000000000000000),
 ( 0.2500000000000000000, 0.2500000000000000000, 0.2999999999999999889, 0.4000000000000000222, 0.5999999999999999778, 1.000000000000000000),
 ( 0.2500000000000000000, 0.2500000000000000000, 0.2999999999999999889, 0.4000000000000000222, 0.5999999999999999778, 1.000000000000000000),
 ( 0.2500000000000000000, 0.2500000000000000000, 0.2999999999999999889, 0.4000000000000000222, 0.5999999999999999778, 1.000000000000000000),
 ( 0.2500000000000000000, 0.2500000000000000000, 0.2999999999999999889, 0.4000000000000000222, 0.5999999999999999778, 1.000000000000000000),
 ( 0.2500000000000000000, 0.2500000000000000000, 0.2999999999999999889, 0.4000000000000000222, 0.5999999999999999778, 1.000000000000000000),
 ( 0.2500000000000000000, 0.2500000000000000000, 0.2999999999999999889, 0.4000000000000000222, 0.5999999999999999778, 1.000000000000000000) ) ) 
 REPRESENTATION_ITEM ( '' )  SURFACE ( )  );
#21403=PRODUCT_DEFINITION_FORMATION_WITH_SPECIFIED_SOURCE ( 'ANY', '', #23487, .NOT_KNOWN. ) ;
#21470=CARTESIAN_POINT ( 'NONE',  ( -2.098672137722010334, -3.287437779826620776, -44.10000000002499121 ) ) ;
#21472=CARTESIAN_POINT ( 'NONE',  ( 5.242919931573567283, -2.735361231296036699, -61.31790713612500099 ) ) ;
#21479=CARTESIAN_POINT ( 'NONE',  ( -2.324326393622344611, -4.567114707776696925, -68.10000000002501963 ) ) ;
#21488=CARTESIAN_POINT ( 'NONE',  ( -1.560798555979769464, 4.306275027539294697, -69.90099036452500059 ) ) ;
#21491=CARTESIAN_POINT ( 'NONE',  ( -0.05052225346893063351, 4.317558364482401601, -57.31818518972499987 ) ) ;
#21522=CARTESIAN_POINT ( 'NONE',  ( -4.178199994060140199, -1.098053884355548737, -56.45102360502500005 ) ) ;
#21565=CARTESIAN_POINT ( 'NONE',  ( 5.943504367937093136, -0.4395870339238064362, -49.60442242802498924 ) ) ;
#21631=CARTESIAN_POINT ( 'NONE',  ( 5.384875807261761516, 2.601783486389667832, -66.85315453642499506 ) ) ;
#21640=CARTESIAN_POINT ( 'NONE',  ( 1.635351980402913297, -4.635989411471753030, -68.10000000002500542 ) ) ;
#21641=CARTESIAN_POINT ( 'NONE',  ( -4.639785291165150483, -1.934394008134929788, -68.10000000002501963 ) ) ;
#21647=CARTESIAN_POINT ( 'NONE',  ( -5.434147616959247529, -3.211087428728324866, -68.32382590962500046 ) ) ;
#21652=CARTESIAN_POINT ( 'NONE',  ( -4.541600168151700423, -0.1148504950298639971, -53.55673954922500002 ) ) ;
#21656=UNCERTAINTY_MEASURE_WITH_UNIT (LENGTH_MEASURE( 1.000000000000000082E-05 ), #620, 'distance_accuracy_value', 'NONE');
#21681=CARTESIAN_POINT ( 'NONE',  ( -5.545418199629476241, -2.237997381628727300, -59.38491726642499202 ) ) ;
#21697=CARTESIAN_POINT ( 'NONE',  ( -2.744417411265728912, -4.298957096598221561, -44.10000000002499121 ) ) ;
#21715=CARTESIAN_POINT ( 'NONE',  ( -2.393684743089945055, 3.904820337558672083, -45.45531229042499888 ) ) ;
#21780=CARTESIAN_POINT ( 'NONE',  ( 0.5814717383643280835, -5.541158915576414046, -67.77495035202500162 ) ) ;
#21796=CARTESIAN_POINT ( 'NONE',  ( -0.9992285280876744835, -5.354791469827751449, -68.70745670422499529 ) ) ;
#21801=CARTESIAN_POINT ( 'NONE',  ( -2.571638601809290936, 3.775240214263654526, -48.05391720702499470 ) ) ;
#21835=CARTESIAN_POINT ( 'NONE',  ( -5.325262776966551037, 2.643762325382846612, -56.79877225282499609 ) ) ;
#21857=CARTESIAN_POINT ( 'NONE',  ( 0.1973057990048258659, -5.030289273761288982, -44.10000000002499121 ) ) ;
#21867=CARTESIAN_POINT ( 'NONE',  ( 3.001777156698443250, -4.698362801289899693, -43.08966640442498885 ) ) ;
#21879=MECHANICAL_DESIGN_GEOMETRIC_PRESENTATION_REPRESENTATION('',(#278),#2754);
#21882=CARTESIAN_POINT ( 'NONE',  ( -4.251243323665415907, -4.132078999800212316, -47.68083066912500101 ) ) ;
#21920=CARTESIAN_POINT ( 'NONE',  ( -4.859832392515191835, 0.02388181653997099169, -44.10000000002499121 ) ) ;
#21944=CARTESIAN_POINT ( 'NONE',  ( 2.776548632478544665, -3.583402058917912747, -52.10430438132500086 ) ) ;
#21948=CARTESIAN_POINT ( 'NONE',  ( -3.151262587278881089, -4.016474153426608851, -68.10000000002501963 ) ) ;
#21954=CARTESIAN_POINT ( 'NONE',  ( -4.475180390489594373, -2.644424941261572126, -69.07382590962501467 ) ) ;
#21961=CARTESIAN_POINT ( 'NONE',  ( 1.082264403401735020, -4.420062499635217357, -64.70397119102501904 ) ) ;
#21965=UNCERTAINTY_MEASURE_WITH_UNIT (LENGTH_MEASURE( 1.000000000000000082E-05 ), #17632, 'distance_accuracy_value', 'NONE');
#21990=CARTESIAN_POINT ( 'NONE',  ( -5.463799992266447525, -1.435916617982112342, -56.45102360502500005 ) ) ;
#22007=CARTESIAN_POINT ( 'NONE',  ( 2.863877650502555383, -3.477044625946443812, -44.10000000002499831 ) ) ;
#22016=CARTESIAN_POINT ( 'NONE',  ( -0.6751951171115599948, 5.935132877056520151, -47.78410749642499411 ) ) ;
#22032=CARTESIAN_POINT ( 'NONE',  ( -0.6751951171115599948, 5.935132877056520151, -48.26410749632500341 ) ) ;
#22069=CARTESIAN_POINT ( 'NONE',  ( -4.689472217220681749, 0.6986887510282764335, -44.10000000002499831 ) ) ;
#22097=CARTESIAN_POINT ( 'NONE',  ( 6.136659917679837761, 0.6935318534637759935, -55.01771407622499765 ) ) ;
#22100=CARTESIAN_POINT ( 'NONE',  ( -4.322343509448423049, 1.111455317196624160, -68.10000000002501963 ) ) ;
#22134=CARTESIAN_POINT ( 'NONE',  ( 1.026682380765238767, -3.915376921412372369, -68.10000000002500542 ) ) ;
#22139=CARTESIAN_POINT ( 'NONE',  ( 3.449241269337446791, -4.803451378176493591, -61.52197827312500067 ) ) ;
#22155=CARTESIAN_POINT ( 'NONE',  ( 2.741601039609154356, -3.445256072409449200, -44.10000000002498410 ) ) ;
#22165=CARTESIAN_POINT ( 'NONE',  ( -3.362912017748242999, 4.936852587875802278, -47.57391720692498893 ) ) ;
#22175=CARTESIAN_POINT ( 'NONE',  ( 4.315256771988532414, 1.538274589489400990, -45.92627377572499370 ) ) ;
#22217=CARTESIAN_POINT ( 'NONE',  ( -4.514398736596065831, 1.028232895072677344, -44.10000000002497700 ) ) ;
#22245=CARTESIAN_POINT ( 'NONE',  ( 2.752605500604612843, 3.655072764488278558, -54.22619010302500442 ) ) ;
#22249=CARTESIAN_POINT ( 'NONE',  ( -4.172593481851767372, 0.2499177695104123076, -68.10000000002499121 ) ) ;
#22293=CARTESIAN_POINT ( 'NONE',  ( -5.941465883516308999, 0.03012783874251079297, -63.05122063482500039 ) ) ;
#22310=CARTESIAN_POINT ( 'NONE',  ( 2.603364185612058179, -3.472772091317404275, -44.10000000002499121 ) ) ;
#22315=PRESENTATION_STYLE_ASSIGNMENT (( #17725 ) ) ;
#22317=CARTESIAN_POINT ( 'NONE',  ( 1.760648636159114933, 4.990344452800529851, -44.74079303332499791 ) ) ;
#22332=CARTESIAN_POINT ( 'NONE',  ( 0.6613659943793989138, -4.850238491497672833, -50.16468436622500349 ) ) ;
#22369=EDGE_LOOP ( 'NONE', ( #22891, #6655 ) ) ;
#22405=CARTESIAN_POINT ( 'NONE',  ( 0.8945918243927786229, -4.819150861182647461, -58.34125695792499045 ) ) ;
#22410=CARTESIAN_POINT ( 'NONE',  ( -4.289535850812038476, 1.058007967770713487, -68.10000000002500542 ) ) ;
#22421=CARTESIAN_POINT ( 'NONE',  ( -4.150389416700803302, 1.923785201099231790, -65.77526299422500244 ) ) ;
#22451=CARTESIAN_POINT ( 'NONE',  ( 4.855544147916073250, 1.989531035200713838, -61.64141554682499446 ) ) ;
#22465=CARTESIAN_POINT ( 'NONE',  ( 2.355191831056934415, -3.552166203893096785, -44.10000000002498410 ) ) ;
#22475=CARTESIAN_POINT ( 'NONE',  ( -1.460566089872938900, -4.291843709425553044, -46.99520033292500187 ) ) ;
#22487=CARTESIAN_POINT ( 'NONE',  ( -4.064488300603595228, -4.392874523441014034, -50.19612412472499585 ) ) ;
#22561=CARTESIAN_POINT ( 'NONE',  ( -5.463799992266447525, -1.435916617982112342, -55.97102360502500318 ) ) ;
#22566=CARTESIAN_POINT ( 'NONE',  ( -4.652080607398097811, 0.7875555626376541385, -68.10000000002500542 ) ) ;
#22574=CARTESIAN_POINT ( 'NONE',  ( -3.351703491987489958, 4.047634511443764183, -62.24933298492499745 ) ) ;
#22587=EDGE_CURVE ( 'NONE', #1473, #29133, #10903, .T. ) ;
#22608=CARTESIAN_POINT ( 'NONE',  ( 4.317698767220935707, -2.252650425851481675, -62.06790713612500099 ) ) ;
#22623=CARTESIAN_POINT ( 'NONE',  ( 1.126323240140575832, -3.906266603841829443, -44.10000000002498410 ) ) ;
#22629=CARTESIAN_POINT ( 'NONE',  ( -4.848570193085766533, 0.4842359979205582143, -47.62737393802499497 ) ) ;
#22639=CARTESIAN_POINT ( 'NONE',  ( 1.728540313474559387, 5.648005006634932990, -51.94125421262499032 ) ) ;
#22704=CARTESIAN_POINT ( 'NONE',  ( 4.824840617521342523, -2.656518825645647119, -57.50843849682499354 ) ) ;
#22711=CARTESIAN_POINT ( 'NONE',  ( -4.184317568092711603, 0.3509751255880352305, -68.10000000002500542 ) ) ;
#22720=CARTESIAN_POINT ( 'NONE',  ( -4.150389416700805079, 1.923785201099232900, -65.37526299422499676 ) ) ;
#22740=CARTESIAN_POINT ( 'NONE',  ( -1.078772944755383767, 5.890544393200768170, -60.25324387862499975 ) ) ;
#22746=CARTESIAN_POINT ( 'NONE',  ( -1.599750255664186049, -3.573568845936323068, -68.10000000002501963 ) ) ;
#22754=CARTESIAN_POINT ( 'NONE',  ( -4.543473910928013559, 0.02303893552233737124, -62.97122063472500031 ) ) ;
#22778=CARTESIAN_POINT ( 'NONE',  ( 1.728540313474559387, 5.648005006634932990, -50.98125421262499657 ) ) ;
#22792=CARTESIAN_POINT ( 'NONE',  ( -4.507646854653408752, 2.674235333181991692, -51.58267869292500052 ) ) ;
#22867=CARTESIAN_POINT ( 'NONE',  ( -4.535753307212162078, -3.367775055652930227, -56.27895058492499913 ) ) ;
#22884=CARTESIAN_POINT ( 'NONE',  ( 2.994727039187459194, -3.426347720743798231, -64.09605006312500564 ) ) ;
#22891=ORIENTED_EDGE ( 'NONE', *, *, #22587, .T. ) ;
#22904=CARTESIAN_POINT ( 'NONE',  ( -3.130203125555106158, 5.106303518385050033, -45.05531229042499319 ) ) ;
#22911=CARTESIAN_POINT ( 'NONE',  ( 2.793573553951601340, -3.441440452430771568, -68.10000000002499121 ) ) ;
#22915=CARTESIAN_POINT ( 'NONE',  ( -4.226820258076031678, 0.7562225394961105129, -44.10000000002500542 ) ) ;
#22919=CARTESIAN_POINT ( 'NONE',  ( 3.609030021535462041, -4.129188278801706247, -65.29605006312499427 ) ) ;
#22942=CARTESIAN_POINT ( 'NONE',  ( -5.649653782182448403, -1.974543963569185046, -50.40743646232499486 ) ) ;
#22952=CARTESIAN_POINT ( 'NONE',  ( 3.630871288588910506, -4.685987307826644965, -52.98430438132500342 ) ) ;
#23025=CARTESIAN_POINT ( 'NONE',  ( -3.468517234904584079, -2.575357395510375902, -55.87895058492500766 ) ) ;
#23044=CARTESIAN_POINT ( 'NONE',  ( -1.746607907818665817, 4.818926816502865584, -68.35099036452500343 ) ) ;
#23063=CARTESIAN_POINT ( 'NONE',  ( 5.643028086411650435, 2.011589847869324377, -45.92627377572500080 ) ) ;
#23071=CARTESIAN_POINT ( 'NONE',  ( 1.895713493160553487, -3.707174971585335488, -68.10000000002500542 ) ) ;
#23078=CARTESIAN_POINT ( 'NONE',  ( -5.973670867983248201, -0.3179945487330332332, -65.56421022022500722 ) ) ;
#23085=CARTESIAN_POINT ( 'NONE',  ( -2.521519673230186775, -3.017545703797773538, -44.16141975532499941 ) ) ;
#23095=CARTESIAN_POINT ( 'NONE',  ( -1.728989203319513779, -3.523396336957824282, -44.10000000002498410 ) ) ;
#23105=CARTESIAN_POINT ( 'NONE',  ( -4.064488300603595228, -4.392874523441014034, -49.71612412472499187 ) ) ;
#23119=CARTESIAN_POINT ( 'NONE',  ( -4.213298386699523945, 4.800796338101376293, -53.98587006832499924 ) ) ;
#23152=CARTESIAN_POINT ( 'NONE',  ( 2.295476649252891743, -3.592865671589301257, -43.96966640442499852 ) ) ;
#23181=CARTESIAN_POINT ( 'NONE',  ( 3.449241269337446791, -4.803451378176493591, -61.04197827312499669 ) ) ;
#23198=CARTESIAN_POINT ( 'NONE',  ( -0.8929276208064895748, -4.785132802852544387, -67.15745670422499813 ) ) ;
#23224=CARTESIAN_POINT ( 'NONE',  ( 1.217040025866600539, -3.881590577319316893, -68.10000000002500542 ) ) ;
#23226=CARTESIAN_POINT ( 'NONE',  ( -4.127468247539838764, -0.07107026465252587466, -44.10000000002499831 ) ) ;
#23230=CARTESIAN_POINT ( 'NONE',  ( 5.384875807261761516, 2.601783486389667832, -67.33315453642501325 ) ) ;
#23256=CARTESIAN_POINT ( 'NONE',  ( -3.108138112192400104, -3.359256988581868608, -49.79612412472500438 ) ) ;
#23267=CARTESIAN_POINT ( 'NONE',  ( -4.541600168151706640, -0.1148504950298593758, -53.95673954922499860 ) ) ;
#23304=CARTESIAN_POINT ( 'NONE',  ( 0.7190444496271986008, -5.886645524271489904, -43.78057807742499818 ) ) ;
#23339=CARTESIAN_POINT ( 'NONE',  ( -5.110483438867316153, -2.062468175234513534, -58.58491726642499486 ) ) ;
#23361=CARTESIAN_POINT ( 'NONE',  ( -0.9992285280876744835, -5.354791469827751449, -67.10745670422500098 ) ) ;
#23385=CARTESIAN_POINT ( 'NONE',  ( -4.535753307212162078, -3.367775055652930227, -56.27895058492499913 ) ) ;
#23391=CARTESIAN_POINT ( 'NONE',  ( 1.954603020853704187, -3.688534106663021284, -68.10000000002501963 ) ) ;
#23393=( GEOMETRIC_REPRESENTATION_CONTEXT ( 3 ) GLOBAL_UNCERTAINTY_ASSIGNED_CONTEXT ( ( #21965 ) ) GLOBAL_UNIT_ASSIGNED_CONTEXT ( ( #17632, #17487, #29913 ) ) REPRESENTATION_CONTEXT ( 'NONE', 'WORKASPACE' ) );
#23399=CARTESIAN_POINT ( 'NONE',  ( 4.883349601227579662, 0.1168011502185895972, -64.46686508972499041 ) ) ;
#23422=CARTESIAN_POINT ( 'NONE',  ( -3.745704904464692842, -4.048335345151853559, -49.39612412472500580 ) ) ;
#23434=CARTESIAN_POINT ( 'NONE',  ( 5.053719932297398465, 0.5711438792955092492, -55.76771407622499055 ) ) ;
#23467=CARTESIAN_POINT ( 'NONE',  ( -4.945984810541346199, -1.782911138613007207, -45.16497819512499490 ) ) ;
#23487=PRODUCT ( 'Catch Spring', 'Catch Spring', '', ( #24392 ) ) ;
#23500=CARTESIAN_POINT ( 'NONE',  ( -4.300317018729668206, 2.364939115720630980, -59.81908057272499946 ) ) ;
#23518=CARTESIAN_POINT ( 'NONE',  ( -5.606848515966891711, 1.848691355091094835, -68.74019511502498858 ) ) ;
#23535=CARTESIAN_POINT ( 'NONE',  ( -1.595193757947241497, 6.212219048941578059, -66.20876360962500939 ) ) ;
#23544=CARTESIAN_POINT ( 'NONE',  ( 2.875056473737671592, -3.558337944997149283, -68.10000000002501963 ) ) ;
#23547=CARTESIAN_POINT ( 'NONE',  ( -2.467959925502309915, -3.051731433341752453, -44.10000000002498410 ) ) ;
#23552=CARTESIAN_POINT ( 'NONE',  ( -4.919493655965280432, -0.2618778636566052032, -66.31421022022500722 ) ) ;
#23579=CARTESIAN_POINT ( 'NONE',  ( -3.985743628842679076, -2.180176701716177057, -53.34982952342500084 ) ) ;
#23588=CARTESIAN_POINT ( 'NONE',  ( -1.256295066205788347, -5.815478746186413694, -55.93033560642499680 ) ) ;
#23653=CARTESIAN_POINT ( 'NONE',  ( 5.433585117924402574, 2.226379967917181180, -60.09141554682499731 ) ) ;
#23669=CARTESIAN_POINT ( 'NONE',  ( -4.185763533044374540, 4.163314928055855901, -68.94322600512501253 ) ) ;
#23687=CARTESIAN_POINT ( 'NONE',  ( -2.744116393020877620, -4.299119443564640264, -68.10000000002500542 ) ) ;
#23729=CARTESIAN_POINT ( 'NONE',  ( -3.469775141984876576, 3.953596984329539321, -53.23587006832500634 ) ) ;
#23738=CARTESIAN_POINT ( 'NONE',  ( 4.692739937114382087, 0.5303478879429707193, -55.41771407622499623 ) ) ;
#23755=CARTESIAN_POINT ( 'NONE',  ( 1.597375353785503327, -4.657940850439431735, -44.10000000002499831 ) ) ;
#23856=CARTESIAN_POINT ( 'NONE',  ( -4.617404660156336327, 1.522451704138575668, -69.49019511502498858 ) ) ;
#23860=CARTESIAN_POINT ( 'NONE',  ( 1.321824945545745145, 4.319062652178982553, -51.46125421262499344 ) ) ;
#23897=CARTESIAN_POINT ( 'NONE',  ( -4.499599993570057244, -1.182519567789861004, -57.20102360502500005 ) ) ;
#23933=CARTESIAN_POINT ( 'NONE',  ( -0.6222386373588042474, 5.469632259241050676, -49.06410749632500057 ) ) ;
#24003=CARTESIAN_POINT ( 'NONE',  ( -4.006504157561272983, -3.130081512437369984, -68.10000000002499121 ) ) ;
#24008=ORIENTED_EDGE ( 'NONE', *, *, #2794, .T. ) ;
#24010=CARTESIAN_POINT ( 'NONE',  ( -0.8291470764733299692, -4.443337602648613327, -67.90745670422499813 ) ) ;
#24014=CARTESIAN_POINT ( 'NONE',  ( 4.009291712408949770, -2.091746824018178685, -61.31790713612500099 ) ) ;
#24042=CARTESIAN_POINT ( 'NONE',  ( 3.992508014903327407, 4.044424149039453908, -58.50805965152499510 ) ) ;
#24061=CARTESIAN_POINT ( 'NONE',  ( -1.728755095528217378, -4.797076482011579657, -44.10000000002499831 ) ) ;
#24081=CARTESIAN_POINT ( 'NONE',  ( 2.137930486642451555, 6.059703978454344941, -45.97079303332500189 ) ) ;
#24148=CARTESIAN_POINT ( 'NONE',  ( 2.402407292417764406, -4.152604782219900592, -68.10000000002501963 ) ) ;
#24149=CARTESIAN_POINT ( 'NONE',  ( -4.505292919096236304, -2.281031367935008269, -68.10000000002500542 ) ) ;
#24156=CARTESIAN_POINT ( 'NONE',  ( -3.200877993934844401, 3.183711413074225671, -69.34322600122500546 ) ) ;
#24160=CARTESIAN_POINT ( 'NONE',  ( 4.883349601227576997, 0.1168011502185872796, -64.06686508972499894 ) ) ;
#24185=ADVANCED_BREP_SHAPE_REPRESENTATION ( '', ( #21218, #17722 ), #23393 ) ;
#24190=CARTESIAN_POINT ( 'NONE',  ( 1.078097839695846494, -5.807694627614346849, -59.54125695792498618 ) ) ;
#24199=COLOUR_RGB ( '', 0.31764706, 0.68627451, 0.89019608) ;
#24226=CARTESIAN_POINT ( 'NONE',  ( 1.760648636159114933, 4.990344452800529851, -46.24079303332500501 ) ) ;
#24294=CARTESIAN_POINT ( 'NONE',  ( -4.541600168151700423, -0.1148504950298639971, -53.55673954922500002 ) ) ;
#24310=CARTESIAN_POINT ( 'NONE',  ( -0.9891938378274525157, -4.753657830815115837, -52.92706695232499925 ) ) ;
#24346=CARTESIAN_POINT ( 'NONE',  ( -3.468517234904584079, -2.575357395510375902, -56.67895058492499061 ) ) ;
#24364=CARTESIAN_POINT ( 'NONE',  ( 2.294646741299938952, -4.244716771087541751, -44.10000000002499121 ) ) ;
#24374=CARTESIAN_POINT ( 'NONE',  ( -3.130203125555106158, 5.106303518385050033, -45.05531229042499319 ) ) ;
#24388=CARTESIAN_POINT ( 'NONE',  ( 2.729852257651755210, -4.492922384981882011, -47.31669147672499776 ) ) ;
#24392=PRODUCT_CONTEXT ( 'NONE', #11779, 'mechanical' ) ;
#24426=CARTESIAN_POINT ( 'NONE',  ( -4.883042975539221509, -0.7801726600661595956, -44.10000000002498410 ) ) ;
#24456=CARTESIAN_POINT ( 'NONE',  ( 0.9406167415663759801, 5.909121140430885433, -53.93500058692499977 ) ) ;
#24460=CARTESIAN_POINT ( 'NONE',  ( -4.556827411881193335, 0.9672853314650907697, -68.10000000002500542 ) ) ;
#24473=CARTESIAN_POINT ( 'NONE',  ( 4.101176313917077820, -1.931410228222282921, -52.29872167392500160 ) ) ;
#24493=CARTESIAN_POINT ( 'NONE',  ( -0.9482832863833026149, -3.805503486056848406, -68.10000000002499121 ) ) ;
#24500=CARTESIAN_POINT ( 'NONE',  ( 5.506968775199813315, -0.09733528975458538568, -58.89793411332500739 ) ) ;
#24518=CARTESIAN_POINT ( 'NONE',  ( 2.821870666190524179, -3.684768625846054135, -44.10000000002499831 ) ) ;
#24526=CARTESIAN_POINT ( 'NONE',  ( 3.314820598666778917, -5.455691467570147779, -46.56669147682499954 ) ) ;
#24540=CARTESIAN_POINT ( 'NONE',  ( 4.432674687120906398, 4.607520344841867121, -49.17426496242499923 ) ) ;
#24580=CARTESIAN_POINT ( 'NONE',  ( -4.827739145450332892, 0.2194149372997978298, -44.10000000002499121 ) ) ;
#24590=( BOUNDED_SURFACE ( )  B_SPLINE_SURFACE ( 5, 5, ( 
 ( #2359, #7377, #26428, #2047, #21236, #2654 ),
 ( #315, #14623, #19182, #12247, #21867, #11941 ),
 ( #29085, #4707, #30989, #9419, #7531, #2203 ),
 ( #30835, #4868, #9894, #7066, #9265, #19026 ),
 ( #28769, #18871, #16656, #28468, #14471, #14156 ),
 ( #11793, #5784, #29392, #7673, #26886, #7829 ),
 ( #20114, #14929, #8129, #10206, #24677, #24374 ),
 ( #3111, #12708, #22317, #2812, #27341, #7981 ),
 ( #24981, #13018, #771, #29852, #1072, #17431 ),
 ( #24833, #19804, #5627, #10662, #10055, #17581 ),
 ( #27036, #15382, #10362, #27189, #19954, #24526 ),
 ( #22475, #19650, #5473, #12404, #924, #29546 ),
 ( #20255, #29233, #17276, #17727, #15080, #15228 ),
 ( #22629, #472, #8287, #17882, #5325, #2964 ),
 ( #3265, #12871, #12557, #27487, #22165, #10515 ),
 ( #3417, #622, #29703, #14772, #22016, #10981 ),
 ( #27809, #25138, #13168, #20734, #3574, #30169 ),
 ( #30007, #6089, #6256, #25623, #15859, #6411 ),
 ( #10828, #3897, #3735, #8601, #13489, #6562 ),
 ( #4055, #18674, #4207, #5933, #25463, #13334 ),
 ( #27968, #23256, #13808, #23422, #23105, #16162 ),
 ( #25776, #1547, #18201, #1852, #11137, #22942 ),
 ( #11452, #15687, #8440, #15533, #30335, #13651 ),
 ( #30498, #1386, #20415, #8764, #18523, #20573 ),
 ( #18373, #16010, #1697, #21051, #22778, #20899 ),
 ( #18039, #11295, #8923, #28125, #25301, #30652 ),
 ( #9078, #1227, #27646, #16624, #7035, #26656 ),
 ( #10135, #21944, #6869, #7760, #26966, #14705 ),
 ( #15011, #30956, #7609, #17203, #2165, #19579 ),
 ( #23579, #395, #26809, #11754, #29313, #5094 ),
 ( #24294, #16471, #19734, #17361, #5253, #2012 ),
 ( #18834, #9383, #23729, #24609, #28436, #14865 ),
 ( #5402, #3041, #9227, #12634, #24456, #9981 ),
 ( #2890, #22245, #12483, #25930, #2742, #702 ),
 ( #554, #29162, #30799, #12338, #18989, #22097 ),
 ( #10292, #28275, #6717, #4365, #21361, #16319 ),
 ( #13968, #4523, #11603, #21201, #28594, #26084 ),
 ( #14121, #10442, #1005, #1471, #8365, #20186 ),
 ( #27420, #23025, #10593, #20340, #5706, #22867 ),
 ( #27728, #1310, #5553, #851, #22561, #5858 ),
 ( #20035, #29778, #7909, #27119, #3500, #17513 ),
 ( #29632, #19892, #29473, #6173, #15773, #8061 ),
 ( #24917, #15156, #25386, #25067, #24758, #10905 ),
 ( #1146, #13249, #27572, #8209, #17811, #17960 ),
 ( #13410, #3193, #20496, #13096, #3824, #15616 ),
 ( #30097, #8524, #15463, #22704, #12798, #10740 ),
 ( #15315, #22405, #17657, #27269, #3343, #29937 ),
 ( #12951, #18125, #6018, #25222, #3652, #9152 ),
 ( #6802, #30574, #28199, #23339, #28356, #21278 ),
 ( #23500, #2089, #1934, #16399, #9002, #6641 ),
 ( #26006, #11062, #30725, #11527, #11679, #21129 ),
 ( #18755, #1622, #4447, #18445, #1782, #30253 ),
 ( #14049, #18602, #20657, #23653, #8682, #18285 ),
 ( #20968, #27892, #6336, #15933, #25541, #28043 ),
 ( #16239, #4294, #3978, #13574, #23181, #11212 ),
 ( #25856, #20814, #11372, #8840, #13889, #30421 ),
 ( #6487, #16088, #25700, #4131, #13728, #25406 ),
 ( #24930, #27134, #3209, #3669, #12964, #3513 ),
 ( #30115, #17526, #22574, #8543, #13271, #5568 ),
 ( #3357, #17829, #5723, #864, #1018, #19903 ),
 ( #15482, #29485, #10605, #10457, #24773, #20052 ),
 ( #27746, #29647, #27283, #15330, #10307, #18143 ),
 ( #3839, #22884, #12817, #13111, #25240, #8381 ),
 ( #20201, #20359, #25082, #13426, #716, #1325 ),
 ( #6192, #27591, #8225, #10920, #20515, #29793 ),
 ( #15793, #27436, #8075, #17670, #7924, #5872 ),
 ( #22421, #22720, #1164, #10759, #15169, #29952 ),
 ( #17980, #6032, #15630, #25719, #9020, #1951 ),
 ( #18929, #30900, #20676, #6506, #21144, #3995 ),
 ( #30440, #25876, #11546, #16106, #9168, #6658 ),
 ( #13593, #18463, #18771, #28528, #20988, #25558 ),
 ( #4152, #4312, #27912, #21296, #8699, #13746 ),
 ( #4466, #18308, #23198, #23361, #18617, #28063 ),
 ( #1800, #11080, #30272, #16256, #6353, #11391 ),
 ( #15951, #1641, #30592, #30738, #28215, #23518 ),
 ( #11229, #13907, #20835, #28379, #6819, #23669 ),
 ( #16415, #4609, #9330, #23044, #26023, #8860 ),
 ( #14065, #2103, #6978, #16567, #11696, #26173 ) ),
 .UNSPECIFIED., .F., .F., .T. ) 
 B_SPLINE_SURFACE_WITH_KNOTS ( ( 6, 3, 3, 3, 3, 3, 3, 3, 3, 3, 3, 3, 3, 3, 3, 3, 3, 3, 3, 3, 3, 3, 3, 3, 3, 6 ),
 ( 6, 6 ),
 ( 0.000000000000000000, 11.49596029219999949, 23.35952330949999833, 35.23214498380000492, 46.71570041140000029, 58.48118637179999979, 70.16173614769999745, 81.99711437660000968, 93.33986353700001359, 104.8204913790000035, 116.3828353250000021, 128.2105526469999859, 137.7231253239999944, 147.2120576640000138, 156.6774103699999898, 168.4624398839999913, 180.2684855139999911, 192.1268167670000082, 203.5147100690000173, 215.0810220189999882, 226.8492753339999979, 238.4740513719999910, 250.2932425120000062, 262.1023078380000015, 273.4723917590000042, 284.7968047250000154 ),
 ( 0.000000000000000000, 6.674405137519999975 ),
 .UNSPECIFIED. ) 
 GEOMETRIC_REPRESENTATION_ITEM ( )  RATIONAL_B_SPLINE_SURFACE ( (
 ( 1.000000000000000000, 0.5999999999999999778, 0.4000000000000000222, 0.2999999999999999889, 0.2500000000000000000, 0.2500000000000000000),
 ( 1.000000000000000000, 0.5999999999999999778, 0.4000000000000000222, 0.2999999999999999889, 0.2500000000000000000, 0.2500000000000000000),
 ( 1.000000000000000000, 0.5999999999999999778, 0.4000000000000000222, 0.2999999999999999889, 0.2500000000000000000, 0.2500000000000000000),
 ( 1.000000000000000000, 0.5999999999999999778, 0.4000000000000000222, 0.2999999999999999889, 0.2500000000000000000, 0.2500000000000000000),
 ( 1.000000000000000000, 0.5999999999999999778, 0.4000000000000000222, 0.2999999999999999889, 0.2500000000000000000, 0.2500000000000000000),
 ( 1.000000000000000000, 0.5999999999999999778, 0.4000000000000000222, 0.2999999999999999889, 0.2500000000000000000, 0.2500000000000000000),
 ( 1.000000000000000000, 0.5999999999999999778, 0.4000000000000000222, 0.2999999999999999889, 0.2500000000000000000, 0.2500000000000000000),
 ( 1.000000000000000000, 0.5999999999999999778, 0.4000000000000000222, 0.2999999999999999889, 0.2500000000000000000, 0.2500000000000000000),
 ( 1.000000000000000000, 0.5999999999999999778, 0.4000000000000000222, 0.2999999999999999889, 0.2500000000000000000, 0.2500000000000000000),
 ( 1.000000000000000000, 0.5999999999999999778, 0.4000000000000000222, 0.2999999999999999889, 0.2500000000000000000, 0.2500000000000000000),
 ( 1.000000000000000000, 0.5999999999999999778, 0.4000000000000000222, 0.2999999999999999889, 0.2500000000000000000, 0.2500000000000000000),
 ( 1.000000000000000000, 0.5999999999999999778, 0.4000000000000000222, 0.2999999999999999889, 0.2500000000000000000, 0.2500000000000000000),
 ( 1.000000000000000000, 0.5999999999999999778, 0.4000000000000000222, 0.2999999999999999889, 0.2500000000000000000, 0.2500000000000000000),
 ( 1.000000000000000000, 0.5999999999999999778, 0.4000000000000000222, 0.2999999999999999889, 0.2500000000000000000, 0.2500000000000000000),
 ( 1.000000000000000000, 0.5999999999999999778, 0.4000000000000000222, 0.2999999999999999889, 0.2500000000000000000, 0.2500000000000000000),
 ( 1.000000000000000000, 0.5999999999999999778, 0.4000000000000000222, 0.2999999999999999889, 0.2500000000000000000, 0.2500000000000000000),
 ( 1.000000000000000000, 0.5999999999999999778, 0.4000000000000000222, 0.2999999999999999889, 0.2500000000000000000, 0.2500000000000000000),
 ( 1.000000000000000000, 0.5999999999999999778, 0.4000000000000000222, 0.2999999999999999889, 0.2500000000000000000, 0.2500000000000000000),
 ( 1.000000000000000000, 0.5999999999999999778, 0.4000000000000000222, 0.2999999999999999889, 0.2500000000000000000, 0.2500000000000000000),
 ( 1.000000000000000000, 0.5999999999999999778, 0.4000000000000000222, 0.2999999999999999889, 0.2500000000000000000, 0.2500000000000000000),
 ( 1.000000000000000000, 0.5999999999999999778, 0.4000000000000000222, 0.2999999999999999889, 0.2500000000000000000, 0.2500000000000000000),
 ( 1.000000000000000000, 0.5999999999999999778, 0.4000000000000000222, 0.2999999999999999889, 0.2500000000000000000, 0.2500000000000000000),
 ( 1.000000000000000000, 0.5999999999999999778, 0.4000000000000000222, 0.2999999999999999889, 0.2500000000000000000, 0.2500000000000000000),
 ( 1.000000000000000000, 0.5999999999999999778, 0.4000000000000000222, 0.2999999999999999889, 0.2500000000000000000, 0.2500000000000000000),
 ( 1.000000000000000000, 0.5999999999999999778, 0.4000000000000000222, 0.2999999999999999889, 0.2500000000000000000, 0.2500000000000000000),
 ( 1.000000000000000000, 0.5999999999999999778, 0.4000000000000000222, 0.2999999999999999889, 0.2500000000000000000, 0.2500000000000000000),
 ( 1.000000000000000000, 0.5999999999999999778, 0.4000000000000000222, 0.2999999999999999889, 0.2500000000000000000, 0.2500000000000000000),
 ( 1.000000000000000000, 0.5999999999999999778, 0.4000000000000000222, 0.2999999999999999889, 0.2500000000000000000, 0.2500000000000000000),
 ( 1.000000000000000000, 0.5999999999999999778, 0.4000000000000000222, 0.2999999999999999889, 0.2500000000000000000, 0.2500000000000000000),
 ( 1.000000000000000000, 0.5999999999999999778, 0.4000000000000000222, 0.2999999999999999889, 0.2500000000000000000, 0.2500000000000000000),
 ( 1.000000000000000000, 0.5999999999999999778, 0.4000000000000000222, 0.2999999999999999889, 0.2500000000000000000, 0.2500000000000000000),
 ( 1.000000000000000000, 0.5999999999999999778, 0.4000000000000000222, 0.2999999999999999889, 0.2500000000000000000, 0.2500000000000000000),
 ( 1.000000000000000000, 0.5999999999999999778, 0.4000000000000000222, 0.2999999999999999889, 0.2500000000000000000, 0.2500000000000000000),
 ( 1.000000000000000000, 0.5999999999999999778, 0.4000000000000000222, 0.2999999999999999889, 0.2500000000000000000, 0.2500000000000000000),
 ( 1.000000000000000000, 0.5999999999999999778, 0.4000000000000000222, 0.2999999999999999889, 0.2500000000000000000, 0.2500000000000000000),
 ( 1.000000000000000000, 0.5999999999999999778, 0.4000000000000000222, 0.2999999999999999889, 0.2500000000000000000, 0.2500000000000000000),
 ( 1.000000000000000000, 0.5999999999999999778, 0.4000000000000000222, 0.2999999999999999889, 0.2500000000000000000, 0.2500000000000000000),
 ( 1.000000000000000000, 0.5999999999999999778, 0.4000000000000000222, 0.2999999999999999889, 0.2500000000000000000, 0.2500000000000000000),
 ( 1.000000000000000000, 0.5999999999999999778, 0.4000000000000000222, 0.2999999999999999889, 0.2500000000000000000, 0.2500000000000000000),
 ( 1.000000000000000000, 0.5999999999999999778, 0.4000000000000000222, 0.2999999999999999889, 0.2500000000000000000, 0.2500000000000000000),
 ( 1.000000000000000000, 0.5999999999999999778, 0.4000000000000000222, 0.2999999999999999889, 0.2500000000000000000, 0.2500000000000000000),
 ( 1.000000000000000000, 0.5999999999999999778, 0.4000000000000000222, 0.2999999999999999889, 0.2500000000000000000, 0.2500000000000000000),
 ( 1.000000000000000000, 0.5999999999999999778, 0.4000000000000000222, 0.2999999999999999889, 0.2500000000000000000, 0.2500000000000000000),
 ( 1.000000000000000000, 0.5999999999999999778, 0.4000000000000000222, 0.2999999999999999889, 0.2500000000000000000, 0.2500000000000000000),
 ( 1.000000000000000000, 0.5999999999999999778, 0.4000000000000000222, 0.2999999999999999889, 0.2500000000000000000, 0.2500000000000000000),
 ( 1.000000000000000000, 0.5999999999999999778, 0.4000000000000000222, 0.2999999999999999889, 0.2500000000000000000, 0.2500000000000000000),
 ( 1.000000000000000000, 0.5999999999999999778, 0.4000000000000000222, 0.2999999999999999889, 0.2500000000000000000, 0.2500000000000000000),
 ( 1.000000000000000000, 0.5999999999999999778, 0.4000000000000000222, 0.2999999999999999889, 0.2500000000000000000, 0.2500000000000000000),
 ( 1.000000000000000000, 0.5999999999999999778, 0.4000000000000000222, 0.2999999999999999889, 0.2500000000000000000, 0.2500000000000000000),
 ( 1.000000000000000000, 0.5999999999999999778, 0.4000000000000000222, 0.2999999999999999889, 0.2500000000000000000, 0.2500000000000000000),
 ( 1.000000000000000000, 0.5999999999999999778, 0.4000000000000000222, 0.2999999999999999889, 0.2500000000000000000, 0.2500000000000000000),
 ( 1.000000000000000000, 0.5999999999999999778, 0.4000000000000000222, 0.2999999999999999889, 0.2500000000000000000, 0.2500000000000000000),
 ( 1.000000000000000000, 0.5999999999999999778, 0.4000000000000000222, 0.2999999999999999889, 0.2500000000000000000, 0.2500000000000000000),
 ( 1.000000000000000000, 0.5999999999999999778, 0.4000000000000000222, 0.2999999999999999889, 0.2500000000000000000, 0.2500000000000000000),
 ( 1.000000000000000000, 0.5999999999999999778, 0.4000000000000000222, 0.2999999999999999889, 0.2500000000000000000, 0.2500000000000000000),
 ( 1.000000000000000000, 0.5999999999999999778, 0.4000000000000000222, 0.2999999999999999889, 0.2500000000000000000, 0.2500000000000000000),
 ( 1.000000000000000000, 0.5999999999999999778, 0.4000000000000000222, 0.2999999999999999889, 0.2500000000000000000, 0.2500000000000000000),
 ( 1.000000000000000000, 0.5999999999999999778, 0.4000000000000000222, 0.2999999999999999889, 0.2500000000000000000, 0.2500000000000000000),
 ( 1.000000000000000000, 0.5999999999999999778, 0.4000000000000000222, 0.2999999999999999889, 0.2500000000000000000, 0.2500000000000000000),
 ( 1.000000000000000000, 0.5999999999999999778, 0.4000000000000000222, 0.2999999999999999889, 0.2500000000000000000, 0.2500000000000000000),
 ( 1.000000000000000000, 0.5999999999999999778, 0.4000000000000000222, 0.2999999999999999889, 0.2500000000000000000, 0.2500000000000000000),
 ( 1.000000000000000000, 0.5999999999999999778, 0.4000000000000000222, 0.2999999999999999889, 0.2500000000000000000, 0.2500000000000000000),
 ( 1.000000000000000000, 0.5999999999999999778, 0.4000000000000000222, 0.2999999999999999889, 0.2500000000000000000, 0.2500000000000000000),
 ( 1.000000000000000000, 0.5999999999999999778, 0.4000000000000000222, 0.2999999999999999889, 0.2500000000000000000, 0.2500000000000000000),
 ( 1.000000000000000000, 0.5999999999999999778, 0.4000000000000000222, 0.2999999999999999889, 0.2500000000000000000, 0.2500000000000000000),
 ( 1.000000000000000000, 0.5999999999999999778, 0.4000000000000000222, 0.2999999999999999889, 0.2500000000000000000, 0.2500000000000000000),
 ( 1.000000000000000000, 0.5999999999999999778, 0.4000000000000000222, 0.2999999999999999889, 0.2500000000000000000, 0.2500000000000000000),
 ( 1.000000000000000000, 0.5999999999999999778, 0.4000000000000000222, 0.2999999999999999889, 0.2500000000000000000, 0.2500000000000000000),
 ( 1.000000000000000000, 0.5999999999999999778, 0.4000000000000000222, 0.2999999999999999889, 0.2500000000000000000, 0.2500000000000000000),
 ( 1.000000000000000000, 0.5999999999999999778, 0.4000000000000000222, 0.2999999999999999889, 0.2500000000000000000, 0.2500000000000000000),
 ( 1.000000000000000000, 0.5999999999999999778, 0.4000000000000000222, 0.2999999999999999889, 0.2500000000000000000, 0.2500000000000000000),
 ( 1.000000000000000000, 0.5999999999999999778, 0.4000000000000000222, 0.2999999999999999889, 0.2500000000000000000, 0.2500000000000000000),
 ( 1.000000000000000000, 0.5999999999999999778, 0.4000000000000000222, 0.2999999999999999889, 0.2500000000000000000, 0.2500000000000000000),
 ( 1.000000000000000000, 0.5999999999999999778, 0.4000000000000000222, 0.2999999999999999889, 0.2500000000000000000, 0.2500000000000000000),
 ( 1.000000000000000000, 0.5999999999999999778, 0.4000000000000000222, 0.2999999999999999889, 0.2500000000000000000, 0.2500000000000000000),
 ( 1.000000000000000000, 0.5999999999999999778, 0.4000000000000000222, 0.2999999999999999889, 0.2500000000000000000, 0.2500000000000000000),
 ( 1.000000000000000000, 0.5999999999999999778, 0.4000000000000000222, 0.2999999999999999889, 0.2500000000000000000, 0.2500000000000000000),
 ( 1.000000000000000000, 0.5999999999999999778, 0.4000000000000000222, 0.2999999999999999889, 0.2500000000000000000, 0.2500000000000000000) ) ) 
 REPRESENTATION_ITEM ( '' )  SURFACE ( )  );
#24609=CARTESIAN_POINT ( 'NONE',  ( -3.882843611328785638, 4.424263292013742799, -53.18587006832499497 ) ) ;
#24612=CARTESIAN_POINT ( 'NONE',  ( -4.296780221824271884, 1.072976733195472931, -68.10000000002501963 ) ) ;
#24653=CARTESIAN_POINT ( 'NONE',  ( 1.094823181362614140, 5.872682718251108547, -63.42744533522500205 ) ) ;
#24668=CARTESIAN_POINT ( 'NONE',  ( 2.753318369310237657, -3.444419153943022671, -44.10000000002499121 ) ) ;
#24677=CARTESIAN_POINT ( 'NONE',  ( -3.130203125555106158, 5.106303518385050033, -44.57531229042499632 ) ) ;
#24688=CARTESIAN_POINT ( 'NONE',  ( 2.776548632478544665, -3.583402058917912747, -52.90430438132499802 ) ) ;
#24758=CARTESIAN_POINT ( 'NONE',  ( -0.06606756225350368661, 5.646037861211643083, -56.83818518972499589 ) ) ;
#24762=CARTESIAN_POINT ( 'NONE',  ( -4.567159517660123846, 0.9507996984954559805, -68.10000000002500542 ) ) ;
#24773=CARTESIAN_POINT ( 'NONE',  ( 3.705709820302785396, 4.685590126413917034, -63.15768011632499679 ) ) ;
#24806=CARTESIAN_POINT ( 'NONE',  ( 4.831710525212951524, -2.520823095555479565, -62.11790713612500525 ) ) ;
#24824=CARTESIAN_POINT ( 'NONE',  ( 2.596444431213495996, -3.474660147395747689, -44.10000000002498410 ) ) ;
#24833=CARTESIAN_POINT ( 'NONE',  ( 4.531630834892032667, -0.6723478992683162847, -46.13818262062499542 ) ) ;
#24849=CARTESIAN_POINT ( 'NONE',  ( 0.8648632234848976363, -6.342619565911398638, -50.24468436622500178 ) ) ;
#24917=CARTESIAN_POINT ( 'NONE',  ( -0.05052225346893063351, 4.317558364482401601, -57.31818518972499987 ) ) ;
#24921=CARTESIAN_POINT ( 'NONE',  ( -4.203413175848027983, 0.5343955542015218496, -68.10000000002501963 ) ) ;
#24930=CARTESIAN_POINT ( 'NONE',  ( -4.543473910928012671, 0.02303893552233621245, -62.57122063472500884 ) ) ;
#24960=CARTESIAN_POINT ( 'NONE',  ( -4.300317018729668206, 2.364939115720640750, -60.21908057272500514 ) ) ;
#24973=CARTESIAN_POINT ( 'NONE',  ( 1.456882742358924565, -3.834140411209185473, -44.10000000002499121 ) ) ;
#24981=CARTESIAN_POINT ( 'NONE',  ( 4.315256771988532414, 1.538274589489400990, -45.92627377572499370 ) ) ;
#24994=CARTESIAN_POINT ( 'NONE',  ( -0.7556487780321572423, 4.453147011089724217, -51.25792092402500089 ) ) ;
#25067=CARTESIAN_POINT ( 'NONE',  ( -0.06088579265679563285, 5.203211362304668519, -56.51818518972498850 ) ) ;
#25073=CARTESIAN_POINT ( 'NONE',  ( -4.468241980872267760, 1.080773483108106614, -68.10000000002501963 ) ) ;
#25082=CARTESIAN_POINT ( 'NONE',  ( 1.165515511291096873, -4.760067307274400861, -63.95397119102499772 ) ) ;
#25102=CARTESIAN_POINT ( 'NONE',  ( 5.363076718300177959, -2.525690298526013677, -52.29872167392500160 ) ) ;
#25110=CARTESIAN_POINT ( 'NONE',  ( 0.1280637868466714679, -3.973485157313911387, -68.10000000002500542 ) ) ;
#25116=CARTESIAN_POINT ( 'NONE',  ( -4.050122923326508584, -2.059172231882750559, -62.36424626872499033 ) ) ;
#25138=CARTESIAN_POINT ( 'NONE',  ( 3.389692407805919849, 3.523397910813145906, -48.29426496242500377 ) ) ;
#25152=CARTESIAN_POINT ( 'NONE',  ( -4.652656055762370180, -1.626095028925849562, -51.15743646232500197 ) ) ;
#25222=CARTESIAN_POINT ( 'NONE',  ( -3.552810942249358117, -4.212879106168850640, -58.37407541852499548 ) ) ;
#25240=CARTESIAN_POINT ( 'NONE',  ( 3.916181512753878824, -4.480608557854155904, -64.01605006312500734 ) ) ;
#25260=CARTESIAN_POINT ( 'NONE',  ( -3.794322484923305705, -3.503605959878534293, -44.22295181582499168 ) ) ;
#25266=CARTESIAN_POINT ( 'NONE',  ( 2.842970026702535513, -3.450524644270692498, -68.10000000002500542 ) ) ;
#25268=CARTESIAN_POINT ( 'NONE',  ( -4.123648947899040351, -0.09406098493378543812, -44.10000000002499121 ) ) ;
#25273=CARTESIAN_POINT ( 'NONE',  ( 4.883349601227576997, 0.1168011502185872796, -64.06686508972499894 ) ) ;
#25301=CARTESIAN_POINT ( 'NONE',  ( 5.782578939028539367, 2.564649547393091478, -51.39998794302498908 ) ) ;
#25311=CARTESIAN_POINT ( 'NONE',  ( 3.630871288588910506, -4.685987307826644965, -52.50430438132499944 ) ) ;
#25386=CARTESIAN_POINT ( 'NONE',  ( -0.05440858064702409902, 4.649678238646714590, -56.56818518972501408 ) ) ;
#25406=CARTESIAN_POINT ( 'NONE',  ( -5.296314592117303377, -2.692763687817543161, -62.36424626872499033 ) ) ;
#25426=CARTESIAN_POINT ( 'NONE',  ( -5.939015604524707115, -0.1501891088408410790, -53.55673954922500002 ) ) ;
#25434=CARTESIAN_POINT ( 'NONE',  ( 2.826807023972331745, -3.676508995340744157, -68.10000000002501963 ) ) ;
#25440=CARTESIAN_POINT ( 'NONE',  ( -4.568101251964848508, -0.2431723019727845825, -65.96421022022501290 ) ) ;
#25463=CARTESIAN_POINT ( 'NONE',  ( 0.8648632234848976363, -6.342619565911398638, -49.28468436622499382 ) ) ;
#25473=CARTESIAN_POINT ( 'NONE',  ( 3.599561039400463347, 4.779710538180673041, -54.62619010302499589 ) ) ;
#25541=CARTESIAN_POINT ( 'NONE',  ( 5.242919931573567283, -2.735361231296036699, -60.83790713612500412 ) ) ;
#25558=CARTESIAN_POINT ( 'NONE',  ( 5.807653394784360934, -2.603268055249425394, -67.27841551502500295 ) ) ;
#25587=CARTESIAN_POINT ( 'NONE',  ( 2.869929429076217620, -3.485336955729469111, -68.10000000002503384 ) ) ;
#25595=CARTESIAN_POINT ( 'NONE',  ( -1.219854050253892153, 4.750520449216608654, -66.60876360982500444 ) ) ;
#25623=CARTESIAN_POINT ( 'NONE',  ( 5.477347162681518000, -0.4051096195737657335, -48.32442242802499521 ) ) ;
#25636=CARTESIAN_POINT ( 'NONE',  ( -5.212126283948660621, -2.851000302232811201, -53.82982952342499061 ) ) ;
#25700=CARTESIAN_POINT ( 'NONE',  ( -4.361670840543652616, -2.217570095850531775, -61.61424626872500454 ) ) ;
#25719=CARTESIAN_POINT ( 'NONE',  ( -1.470080522021702363, 5.724986182348157371, -65.40876360972499981 ) ) ;
#25735=CARTESIAN_POINT ( 'NONE',  ( -5.325262776966551037, 2.643762325382846612, -56.79877225282499609 ) ) ;
#25743=CARTESIAN_POINT ( 'NONE',  ( 2.865660253176993688, -3.596091862522109661, -68.10000000002500542 ) ) ;
#25747=CARTESIAN_POINT ( 'NONE',  ( -4.120143249015659315, -0.1148328759544282596, -44.10000000002499121 ) ) ;
#25751=CARTESIAN_POINT ( 'NONE',  ( 5.807653394784360934, -2.603268055249425394, -67.75841551502499271 ) ) ;
#25767=CARTESIAN_POINT ( 'NONE',  ( -0.6975711794063483850, -3.867593748343274740, -44.10000000002499121 ) ) ;
#25773=AXIS2_PLACEMENT_3D ( 'NONE', #20087, #1044, #8573 ) ;
#25776=CARTESIAN_POINT ( 'NONE',  ( -4.320323480314920417, -1.509945384023513082, -50.40743646232499486 ) ) ;
#25786=CARTESIAN_POINT ( 'NONE',  ( -4.541600168151700423, -0.1148504950298639971, -53.55673954922500002 ) ) ;
#25825=CARTESIAN_POINT ( 'NONE',  ( -1.557622931652909104, -4.259165208650869339, -43.98640794712500224 ) ) ;
#25856=CARTESIAN_POINT ( 'NONE',  ( -1.143212971672622036, -4.711439499498762729, -61.94311227092499195 ) ) ;
#25865=CARTESIAN_POINT ( 'NONE',  ( -3.901237024542355769, -0.9768880954038594577, -68.10000000002501963 ) ) ;
#25876=CARTESIAN_POINT ( 'NONE',  ( 4.117846205589238195, 1.989599136607399954, -66.45315453652499116 ) ) ;
#25894=CARTESIAN_POINT ( 'NONE',  ( 3.916181512753878824, -4.480608557854155904, -64.49605006312501132 ) ) ;
#25900=CARTESIAN_POINT ( 'NONE',  ( 2.814735968722008153, -3.697461604360650522, -68.10000000002499121 ) ) ;
#25905=CARTESIAN_POINT ( 'NONE',  ( -4.125964278595938950, -0.08019631128595877678, -44.10000000002500542 ) ) ;
#25908=CARTESIAN_POINT ( 'NONE',  ( -4.150389416700805079, 1.923785201099232900, -66.17526299432499570 ) ) ;
#25930=CARTESIAN_POINT ( 'NONE',  ( 3.317242526492594212, 4.404831280259204895, -53.82619010302499873 ) ) ;
#25938=CARTESIAN_POINT ( 'NONE',  ( 2.097865490181839654, -3.779070126327678025, -55.98172062782500547 ) ) ;
#25976=CARTESIAN_POINT ( 'NONE',  ( -5.162912894389027230, 3.035924517800103750, -44.84354844312500177 ) ) ;
#26006=CARTESIAN_POINT ( 'NONE',  ( -0.8249440165340113928, 4.504533947698903695, -60.25324387862499975 ) ) ;
#26019=ORIENTED_EDGE ( 'NONE', *, *, #17309, .T. ) ;
#26023=CARTESIAN_POINT ( 'NONE',  ( -1.895255389310859684, 5.229048247678121264, -68.67099036452499661 ) ) ;
#26045=CARTESIAN_POINT ( 'NONE',  ( 1.094823181362614140, 5.872682718251108547, -63.42744533522500205 ) ) ;
#26052=CARTESIAN_POINT ( 'NONE',  ( 1.576770949147058731, -4.662922928932242250, -68.10000000002500542 ) ) ;
#26084=CARTESIAN_POINT ( 'NONE',  ( 2.743362564037614248, -4.941860934411918649, -55.58172062782499268 ) ) ;
#26094=CARTESIAN_POINT ( 'NONE',  ( 2.528196872781957705, -4.554263998399506796, -56.38172062782499694 ) ) ;
#26130=CARTESIAN_POINT ( 'NONE',  ( -2.884696998040799709, 4.705809124755043982, -45.85531229042501167 ) ) ;
#26173=CARTESIAN_POINT ( 'NONE',  ( 0.3196029497759475535, 5.089975830446680227, -69.35875473022500159 ) ) ;
#26194=CARTESIAN_POINT ( 'NONE',  ( -5.941465883516308999, 0.03012783874251079297, -62.57122063482501062 ) ) ;
#26209=CARTESIAN_POINT ( 'NONE',  ( 4.441146713720570460, -1.990734395216660069, -67.67841551502500863 ) ) ;
#26213=CARTESIAN_POINT ( 'NONE',  ( -1.219854050253890598, 4.750520449216602437, -66.20876360982499875 ) ) ;
#26247=CARTESIAN_POINT ( 'NONE',  ( -0.05052225346893063351, 4.317558364482401601, -57.31818518972499987 ) ) ;
#26280=CARTESIAN_POINT ( 'NONE',  ( -3.362912017748242999, 4.936852587875802278, -48.53391720692499689 ) ) ;
#26360=CARTESIAN_POINT ( 'NONE',  ( 1.409024965274377150, -4.735590434768029766, -68.10000000002503384 ) ) ;
#26368=CARTESIAN_POINT ( 'NONE',  ( -1.084269253894827534, -5.810518403417324507, -67.90745670422499813 ) ) ;
#26373=CARTESIAN_POINT ( 'NONE',  ( 4.508719565894415915, 1.847421675581904843, -60.89141554682500157 ) ) ;
#26403=CARTESIAN_POINT ( 'NONE',  ( 4.003591150705128499, -2.204345408526048988, -58.70843849682500348 ) ) ;
#26428=CARTESIAN_POINT ( 'NONE',  ( 3.498556269673057884, -2.323812390827893815, -42.60875473022500159 ) ) ;
#26438=CARTESIAN_POINT ( 'NONE',  ( 3.650437977654107602, 3.794428519304413605, -49.44426496242500235 ) ) ;
#26504=CARTESIAN_POINT ( 'NONE',  ( 0.7004501677642104296, -4.947957971645007724, -68.10000000002501963 ) ) ;
#26514=CARTESIAN_POINT ( 'NONE',  ( 0.2632024292269652954, 4.191744801550177257, -70.10875473022500159 ) ) ;
#26520=CARTESIAN_POINT ( 'NONE',  ( -3.221934060409652023, 3.671197199744479001, -53.98587006832499924 ) ) ;
#26551=CARTESIAN_POINT ( 'NONE',  ( -0.05052225346893526176, 4.317558364482406930, -57.71818518972499845 ) ) ;
#26567=CARTESIAN_POINT ( 'NONE',  ( -2.118729980851755901, -4.637508198188047714, -44.10000000002499121 ) ) ;
#26589=CARTESIAN_POINT ( 'NONE',  ( -1.909971040720825908, -5.612411004515823088, -46.99520033292500187 ) ) ;
#26656=CARTESIAN_POINT ( 'NONE',  ( 5.363076718300177959, -2.525690298526013677, -52.29872167392500160 ) ) ;
#26658=CARTESIAN_POINT ( 'NONE',  ( 2.471021819916508822, -4.092477270420384450, -68.10000000002504805 ) ) ;
#26664=CARTESIAN_POINT ( 'NONE',  ( 1.257215589593047023, -4.341675124665348662, -68.10367649352500052 ) ) ;
#26669=CARTESIAN_POINT ( 'NONE',  ( -2.948077164825084306, -3.495793300896363753, -59.17407541852499975 ) ) ;
#26698=CARTESIAN_POINT ( 'NONE',  ( 4.332295931058598448, 4.388630459628991787, -57.70805965152499795 ) ) ;
#26716=CARTESIAN_POINT ( 'NONE',  ( 2.541294302003115568, -4.027761424469836093, -44.10000000002499121 ) ) ;
#26736=CARTESIAN_POINT ( 'NONE',  ( -5.221537131022022216, 0.5214849208526588509, -48.37737393802499497 ) ) ;
#26777=CARTESIAN_POINT ( 'NONE',  ( -4.647753910737981720, 0.7988342186384705945, -44.10000000002498410 ) ) ;
#26809=CARTESIAN_POINT ( 'NONE',  ( -4.292339292658051697, -2.347882601813513492, -52.59982952342499374 ) ) ;
#26812=CARTESIAN_POINT ( 'NONE',  ( -4.059731841906703664, -0.4201311362673507133, -68.10000000002501963 ) ) ;
#26824=CARTESIAN_POINT ( 'NONE',  ( 2.097865490181829884, -3.779070126327673140, -55.58172062782499268 ) ) ;
#26858=CARTESIAN_POINT ( 'NONE',  ( -5.035266659556940638, -1.323295706752037670, -57.25102360502499721 ) ) ;
#26877=CARTESIAN_POINT ( 'NONE',  ( 0.4822354468651134929, -3.969360884996547156, -44.10000000002497700 ) ) ;
#26886=CARTESIAN_POINT ( 'NONE',  ( -5.162912894389027230, 3.035924517800103750, -44.36354844312499779 ) ) ;
#26899=CARTESIAN_POINT ( 'NONE',  ( -4.848570193085772750, 0.4842359979205512754, -48.02737393802500065 ) ) ;
#26940=CARTESIAN_POINT ( 'NONE',  ( -4.328334940905476991, -2.689252967667119520, -44.10000000002499121 ) ) ;
#26966=CARTESIAN_POINT ( 'NONE',  ( 3.630871288588910506, -4.685987307826644965, -52.02430438132500257 ) ) ;
#26970=CARTESIAN_POINT ( 'NONE',  ( -4.660805219281239253, 0.7680161694985663257, -68.10000000002503384 ) ) ;
#27011=CARTESIAN_POINT ( 'NONE',  ( -4.069925668896384963, 4.914984763948436530, -63.47933298482501385 ) ) ;
#27029=CARTESIAN_POINT ( 'NONE',  ( 2.877784302101842773, -3.523144701061436734, -44.10000000002499831 ) ) ;
#27036=CARTESIAN_POINT ( 'NONE',  ( 2.534862810676351330, -4.171999357468124003, -46.56669147672499065 ) ) ;
#27050=CARTESIAN_POINT ( 'NONE',  ( 5.066518387468507356, -3.138291312573631586, -49.33324460762499797 ) ) ;
#27092=PRESENTATION_STYLE_ASSIGNMENT (( #5528 ) ) ;
#27119=CARTESIAN_POINT ( 'NONE',  ( -4.907595108195073941, 2.436408417514825953, -55.99877225282499182 ) ) ;
#27124=CARTESIAN_POINT ( 'NONE',  ( -4.078087104978500577, -0.3378962543220449533, -68.10000000002501963 ) ) ;
#27134=CARTESIAN_POINT ( 'NONE',  ( -4.543473910928013559, 0.02303893552233737124, -62.17122063472501026 ) ) ;
#27167=CARTESIAN_POINT ( 'NONE',  ( 2.637655088286918748, -3.673227524439518277, -61.92197827312500635 ) ) ;
#27180=CARTESIAN_POINT ( 'NONE',  ( 2.047979779693930524, -3.657782141751653615, -44.10000000002499121 ) ) ;
#27189=CARTESIAN_POINT ( 'NONE',  ( 3.054834669310706907, -5.027794097514915350, -45.76669147682500238 ) ) ;
#27202=CARTESIAN_POINT ( 'NONE',  ( 5.782578939028539367, 2.564649547393091478, -52.35998794302499704 ) ) ;
#27241=FILL_AREA_STYLE ('',( #825 ) ) ;
#27269=CARTESIAN_POINT ( 'NONE',  ( 1.078097839695846494, -5.807694627614346849, -57.94125695792499897 ) ) ;
#27274=CARTESIAN_POINT ( 'NONE',  ( -4.205306023310510177, 0.5530484625032894286, -68.10000000002501963 ) ) ;
#27283=CARTESIAN_POINT ( 'NONE',  ( 5.258991878263315378, 0.1257858540645254708, -63.31686508972500604 ) ) ;
#27318=CARTESIAN_POINT ( 'NONE',  ( 3.449241269337446791, -4.803451378176493591, -62.00197827312499754 ) ) ;
#27335=CARTESIAN_POINT ( 'NONE',  ( 1.694282209123973093, -3.767548914987134623, -44.10000000002498410 ) ) ;
#27341=CARTESIAN_POINT ( 'NONE',  ( 2.137930486642451555, 6.059703978454344941, -45.01079303332499393 ) ) ;
#27355=CARTESIAN_POINT ( 'NONE',  ( 3.874396413951479268, -2.399869827310083803, -49.33324460762499797 ) ) ;
#27397=SHAPE_REPRESENTATION_RELATIONSHIP ( 'NONE' , 'NONE' ,  #19806, #24185 ) ;
#27420=CARTESIAN_POINT ( 'NONE',  ( -3.468517234904579194, -2.575357395510371461, -56.27895058492499913 ) ) ;
#27426=CARTESIAN_POINT ( 'NONE',  ( -4.304922296158920858, 1.087454836608482855, -68.10000000002500542 ) ) ;
#27436=CARTESIAN_POINT ( 'NONE',  ( -4.568101251970387189, -0.2431723019811170283, -65.16421022022500154 ) ) ;
#27450=CARTESIAN_POINT ( 'NONE',  ( -5.623491485972666126, 3.092612689740418919, -59.81908057272499946 ) ) ;
#27465=CARTESIAN_POINT ( 'NONE',  ( 2.637655088286928962, -3.673227524439524050, -61.52197827312500067 ) ) ;
#27487=CARTESIAN_POINT ( 'NONE',  ( -3.099154212379724882, 4.549648463301534385, -47.25391720692500286 ) ) ;
#27500=CARTESIAN_POINT ( 'NONE',  ( 4.894650655971835462, -0.3620128515310818140, -49.87442242802501369 ) ) ;
#27572=CARTESIAN_POINT ( 'NONE',  ( 3.567773119718944397, 3.614166260817118559, -56.95805965152499084 ) ) ;
#27581=CARTESIAN_POINT ( 'NONE',  ( -4.041264224475901834, -0.4991584895587213300, -68.10000000002499121 ) ) ;
#27591=CARTESIAN_POINT ( 'NONE',  ( -2.911316102855189492, -3.927725552494646166, -64.73409070562500744 ) ) ;
#27608=CARTESIAN_POINT ( 'NONE',  ( 5.925978784015399903, -0.8792241758803844842, -46.13818262062499542 ) ) ;
#27621=CARTESIAN_POINT ( 'NONE',  ( -1.143212971672622036, -4.711439499498762729, -61.94311227092499195 ) ) ;
#27646=CARTESIAN_POINT ( 'NONE',  ( 4.416651415012724513, -2.079980245798425109, -51.54872167392500870 ) ) ;
#27658=CARTESIAN_POINT ( 'NONE',  ( 1.423503787547387933, 4.651298240777052229, -52.21125421252499876 ) ) ;
#27673=DIRECTION ( 'NONE',  ( -0.8329895880221872551, 0.5532886644841250590, 0.000000000000000000 ) ) ;
#27728=CARTESIAN_POINT ( 'NONE',  ( -4.178199994060140199, -1.098053884355548737, -56.45102360502500005 ) ) ;
#27746=CARTESIAN_POINT ( 'NONE',  ( 4.883349601227576997, 0.1168011502185872796, -64.06686508972499894 ) ) ;
#27766=CARTESIAN_POINT ( 'NONE',  ( -3.362912017748242999, 4.936852587875802278, -48.05391720702499470 ) ) ;
#27772=CARTESIAN_POINT ( 'NONE',  ( 2.746170412676653072, -3.444806756781638502, -68.10000000002500542 ) ) ;
#27780=CARTESIAN_POINT ( 'NONE',  ( -2.911316102860717070, -3.927725552502972839, -65.53409070562500460 ) ) ;
#27797=CARTESIAN_POINT ( 'NONE',  ( -0.8022125085872947592, -3.843042093354096078, -44.10000000002498410 ) ) ;
#27809=CARTESIAN_POINT ( 'NONE',  ( 3.389692407805913632, 3.523397910813151679, -48.69426496242499525 ) ) ;
#27817=CARTESIAN_POINT ( 'NONE',  ( -0.9606962270921419744, -4.447130805931738706, -56.33033560642500248 ) ) ;
#27892=CARTESIAN_POINT ( 'NONE',  ( 4.009291712408942665, -2.091746824018185347, -60.91790713612499530 ) ) ;
#27900=CARTESIAN_POINT ( 'NONE',  ( -3.957406504849845241, -0.8124326615230210713, -68.10000000002500542 ) ) ;
#27912=CARTESIAN_POINT ( 'NONE',  ( 1.353924481083393028, -4.675650134241364775, -66.95367649362499662 ) ) ;
#27938=CARTESIAN_POINT ( 'NONE',  ( 1.858630010972899704, -3.718756527810015644, -68.10000000002501963 ) ) ;
#27941=CARTESIAN_POINT ( 'NONE',  ( -3.694857771750023279, -1.477660183791897008, -44.10000000002497700 ) ) ;
#27945=CARTESIAN_POINT ( 'NONE',  ( 3.705709820302785396, 4.685590126413917034, -64.11768011632500475 ) ) ;
#27968=CARTESIAN_POINT ( 'NONE',  ( -3.108138112192390778, -3.359256988581870385, -50.19612412472499585 ) ) ;
#27979=CARTESIAN_POINT ( 'NONE',  ( -5.939015604524707115, -0.1501891088408410790, -54.03673954922499689 ) ) ;
#27992=DIRECTION ( 'NONE',  ( 0.000000000000000000, 0.000000000000000000, -1.000000000000000000 ) ) ;
#28043=CARTESIAN_POINT ( 'NONE',  ( 5.242919931573567283, -2.735361231296036699, -61.31790713612500099 ) ) ;
#28063=CARTESIAN_POINT ( 'NONE',  ( -1.084269253894827534, -5.810518403417324507, -67.90745670422499813 ) ) ;
#28081=CARTESIAN_POINT ( 'NONE',  ( 1.169850847344618083, -6.301966510834352775, -58.74125695792500323 ) ) ;
#28089=CARTESIAN_POINT ( 'NONE',  ( 2.132677846510928177, -3.629065541562336961, -68.10000000002500542 ) ) ;
#28094=CARTESIAN_POINT ( 'NONE',  ( -3.753535784774050921, -1.349497875818973291, -44.10000000002498410 ) ) ;
#28098=CARTESIAN_POINT ( 'NONE',  ( 2.708949881112997282, 3.684664522020660193, -66.64226422532500749 ) ) ;
#28125=CARTESIAN_POINT ( 'NONE',  ( 5.329043336022200705, 2.363500563244980590, -51.07998794302500301 ) ) ;
#28135=CARTESIAN_POINT ( 'NONE',  ( -4.292339292658051697, -2.347882601813513492, -54.09982952342500084 ) ) ;
#28171=CARTESIAN_POINT ( 'NONE',  ( -6.005838698572866008, -2.164963525412170853, -44.41497819512499490 ) ) ;
#28199=CARTESIAN_POINT ( 'NONE',  ( -4.566814987872939824, -1.843056667269423743, -58.63491726642500623 ) ) ;
#28215=CARTESIAN_POINT ( 'NONE',  ( -5.606848515966891711, 1.848691355091094835, -68.26019511502499881 ) ) ;
#28240=CARTESIAN_POINT ( 'NONE',  ( 2.408015917153201180, -3.534003425642091578, -68.10000000002500542 ) ) ;
#28243=CARTESIAN_POINT ( 'NONE',  ( -2.098672137722010334, -3.287437779826620776, -44.10000000002499121 ) ) ;
#28248=CARTESIAN_POINT ( 'NONE',  ( 1.082264403401723474, -4.420062499635215580, -65.10397119102499630 ) ) ;
#28275=CARTESIAN_POINT ( 'NONE',  ( 3.357378826392681592, -2.722208303785305539, -55.00923804942500084 ) ) ;
#28285=CARTESIAN_POINT ( 'NONE',  ( 2.259239758627727745, -4.069767828330737913, -56.33172062782499978 ) ) ;
#28324=CARTESIAN_POINT ( 'NONE',  ( -3.948109860491266776, 2.321589337205137937, -45.24354844312500745 ) ) ;
#28356=CARTESIAN_POINT ( 'NONE',  ( -5.545418199629476241, -2.237997381628727300, -58.90491726642499515 ) ) ;
#28379=CARTESIAN_POINT ( 'NONE',  ( -3.857468353316018117, 3.836780423039637178, -68.14322600472499403 ) ) ;
#28399=CARTESIAN_POINT ( 'NONE',  ( 3.542472921321142110, 4.818407451951889797, -66.64226422552501106 ) ) ;
#28406=CARTESIAN_POINT ( 'NONE',  ( 2.495111619170718775, -4.070681774061544189, -68.10000000002501963 ) ) ;
#28413=CARTESIAN_POINT ( 'NONE',  ( 3.542472921321142110, 4.818407451951889797, -67.12226422552500082 ) ) ;
#28436=CARTESIAN_POINT ( 'NONE',  ( -4.213298386699523945, 4.800796338101376293, -53.50587006832499526 ) ) ;
#28445=CARTESIAN_POINT ( 'NONE',  ( -1.034595936873321076, -4.789217790999566127, -56.68033560642500390 ) ) ;
#28468=CARTESIAN_POINT ( 'NONE',  ( -5.534792526179823646, -1.995162464570431782, -43.61497819512499774 ) ) ;
#28480=CARTESIAN_POINT ( 'NONE',  ( -3.130203125555106158, 5.106303518385050033, -45.05531229042499319 ) ) ;
#28528=CARTESIAN_POINT ( 'NONE',  ( 5.352151167820474953, -2.399090168605950701, -66.47841551492498979 ) ) ;
#28563=CARTESIAN_POINT ( 'NONE',  ( -3.519556364420927785, -3.690466755798151866, -68.10000000002500542 ) ) ;
#28565=CARTESIAN_POINT ( 'NONE',  ( -4.850149637780369893, 0.09109815604563743785, -44.10000000002497700 ) ) ;
#28569=CARTESIAN_POINT ( 'NONE',  ( -4.155524648305278568, -2.455537445457761869, -68.32382590962500046 ) ) ;
#28573=CARTESIAN_POINT ( 'NONE',  ( -4.320323480314920417, -1.509945384023513082, -50.40743646232499486 ) ) ;
#28594=CARTESIAN_POINT ( 'NONE',  ( 2.743362564037614248, -4.941860934411918649, -55.10172062782499580 ) ) ;
#28605=CARTESIAN_POINT ( 'NONE',  ( -1.777987283592920020, 4.296653259772734046, -57.89652090042500276 ) ) ;
#28710=CARTESIAN_POINT ( 'NONE',  ( -2.744116393020877620, -4.299119443564640264, -68.10000000002500542 ) ) ;
#28716=CARTESIAN_POINT ( 'NONE',  ( 0.3196029497759475535, 5.089975830446680227, -69.83875473022500557 ) ) ;
#28722=CARTESIAN_POINT ( 'NONE',  ( 0.8945918243927832858, -4.819150861182647461, -58.74125695792500323 ) ) ;
#28746=CARTESIAN_POINT ( 'NONE',  ( -1.989652436383612555, 4.808159600214577445, -57.94652090042499992 ) ) ;
#28769=CARTESIAN_POINT ( 'NONE',  ( -4.592700181227121980, -1.655560342997616896, -44.41497819512500200 ) ) ;
#28781=CARTESIAN_POINT ( 'NONE',  ( -1.460566089872938900, -4.291843709425553044, -46.99520033292500187 ) ) ;
#28847=CARTESIAN_POINT ( 'NONE',  ( 2.473875800322225427, -5.003071188766746502, -67.61367454182500580 ) ) ;
#28860=CARTESIAN_POINT ( 'NONE',  ( -2.744116393020877620, -4.299119443564640264, -68.10000000002500542 ) ) ;
#28861=CARTESIAN_POINT ( 'NONE',  ( -4.147568857911904772, -2.928510985069560757, -68.10000000002500542 ) ) ;
#28867=APPLICATION_CONTEXT ( 'automotive_design' ) ;
#28876=CARTESIAN_POINT ( 'NONE',  ( 0.7192951553254764985, 4.518739695583327887, -54.41500058692499664 ) ) ;
#28883=UNCERTAINTY_MEASURE_WITH_UNIT (LENGTH_MEASURE( 1.000000000000000082E-05 ), #14838, 'distance_accuracy_value', 'NONE');
#28909=CARTESIAN_POINT ( 'NONE',  ( -4.240613917342963113, -1.711409762446096439, -59.38491726642499202 ) ) ;
#28947=CARTESIAN_POINT ( 'NONE',  ( 1.970249664213433727, 5.584433078155761621, -46.29079303332500217 ) ) ;
#29015=CARTESIAN_POINT ( 'NONE',  ( -4.834657140208623360, 0.1770554249713849337, -68.10000000002501963 ) ) ;
#29027=CARTESIAN_POINT ( 'NONE',  ( -4.185672079393978784, 2.483218523716627768, -50.83267869292499341 ) ) ;
#29061=CARTESIAN_POINT ( 'NONE',  ( 5.975646968830259809, -0.1056191442178888718, -58.09793411332499602 ) ) ;
#29085=CARTESIAN_POINT ( 'NONE',  ( 0.5498575204270217398, -4.501552459765377101, -43.78057807742499818 ) ) ;
#29096=CARTESIAN_POINT ( 'NONE',  ( 4.647199600633202365, 1.656603404052558348, -46.67627377572500791 ) ) ;
#29133=VERTEX_POINT ( 'NONE', #2698 ) ;
#29162=CARTESIAN_POINT ( 'NONE',  ( 4.692739937119916327, 0.5303478879513032762, -54.61771407622499197 ) ) ;
#29165=CARTESIAN_POINT ( 'NONE',  ( -3.691491291332746449, -3.512112988921174850, -68.10000000002500542 ) ) ;
#29171=CARTESIAN_POINT ( 'NONE',  ( -1.084269253894827534, -5.810518403417324507, -68.38745670422500211 ) ) ;
#29175=CARTESIAN_POINT ( 'NONE',  ( -2.393684743089937061, 3.904820337558664978, -45.05531229042499319 ) ) ;
#29203=DIRECTION ( 'NONE',  ( 1.000000000000000000, 0.000000000000000000, 0.000000000000000000 ) ) ;
#29205=CARTESIAN_POINT ( 'NONE',  ( 5.975646968830259809, -0.1056191442178888718, -58.57793411332500000 ) ) ;
#29225=CARTESIAN_POINT ( 'NONE',  ( 1.704222867702336552, -3.764723383760178343, -44.10000000002499831 ) ) ;
#29233=CARTESIAN_POINT ( 'NONE',  ( -3.250950776947242993, -3.159825117472811140, -46.80083066912501266 ) ) ;
#29246=CARTESIAN_POINT ( 'NONE',  ( 4.432674687120906398, 4.607520344841867121, -48.69426496242499525 ) ) ;
#29287=CARTESIAN_POINT ( 'NONE',  ( -4.523686073471028024, 1.015938900863429195, -44.10000000002499831 ) ) ;
#29313=CARTESIAN_POINT ( 'NONE',  ( -5.212126283948660621, -2.851000302232811201, -52.86982952342499686 ) ) ;
#29318=CARTESIAN_POINT ( 'NONE',  ( -4.361734194508183116, 1.139633373421352402, -68.10000000002500542 ) ) ;
#29363=CARTESIAN_POINT ( 'NONE',  ( -4.050122923326521018, -2.059172231882739457, -62.76424626872500312 ) ) ;
#29383=CARTESIAN_POINT ( 'NONE',  ( 2.636753967748677763, -3.464035022006507702, -44.10000000002499121 ) ) ;
#29392=CARTESIAN_POINT ( 'NONE',  ( -4.251810618965843780, 2.500173132353668226, -44.09354844312500177 ) ) ;
#29404=CARTESIAN_POINT ( 'NONE',  ( 3.874396413951474827, -2.399869827310081583, -49.73324460762500365 ) ) ;
#29444=CARTESIAN_POINT ( 'NONE',  ( -4.895342878087565630, -0.3722554304256932567, -44.10000000002499121 ) ) ;
#29473=CARTESIAN_POINT ( 'NONE',  ( -1.777987283592920020, 4.296653259772734046, -56.39652090042499566 ) ) ;
#29478=CARTESIAN_POINT ( 'NONE',  ( -4.235963752770566693, 0.8297158020410684287, -68.10000000002500542 ) ) ;
#29485=CARTESIAN_POINT ( 'NONE',  ( 2.833778097863423717, 3.583098331959791771, -63.23768011632500219 ) ) ;
#29520=CARTESIAN_POINT ( 'NONE',  ( -4.892971904093138313, 0.02481116134537240947, -63.32122063472500173 ) ) ;
#29539=CARTESIAN_POINT ( 'NONE',  ( 2.319980218398844940, -3.564287903756054199, -44.10000000002499831 ) ) ;
#29546=CARTESIAN_POINT ( 'NONE',  ( -1.909971040720825908, -5.612411004515823088, -46.99520033292500187 ) ) ;
#29560=CARTESIAN_POINT ( 'NONE',  ( -4.185672079393965461, 2.483218523716621107, -51.23267869292500620 ) ) ;
#29632=CARTESIAN_POINT ( 'NONE',  ( -1.650988191866306742, 3.989749455477753504, -57.14652090042499566 ) ) ;
#29639=CARTESIAN_POINT ( 'NONE',  ( -4.403294653383551527, 1.129803870268460075, -68.10000000002499121 ) ) ;
#29647=CARTESIAN_POINT ( 'NONE',  ( 4.883349601227579662, 0.1168011502185895972, -63.66686508972499325 ) ) ;
#29681=CARTESIAN_POINT ( 'NONE',  ( 1.094823181362614140, 5.872682718251108547, -63.90744533522500603 ) ) ;
#29695=CARTESIAN_POINT ( 'NONE',  ( 1.984258505993609978, -3.678877725158681944, -44.10000000002499831 ) ) ;
#29703=CARTESIAN_POINT ( 'NONE',  ( -0.5560430376289927645, 4.887756486939889733, -47.51410749632499630 ) ) ;
#29715=CARTESIAN_POINT ( 'NONE',  ( 4.545032752014871669, -0.3361547907463971474, -49.12442242802499237 ) ) ;
#29778=CARTESIAN_POINT ( 'NONE',  ( -4.072259770650996202, 2.021700601780457962, -56.39877225282500461 ) ) ;
#29784=CARTESIAN_POINT ( 'NONE',  ( -4.195251052989737772, 0.4538500998018956123, -68.10000000002501963 ) ) ;
#29793=CARTESIAN_POINT ( 'NONE',  ( -3.807105672873282831, -5.136256491778199873, -65.13409070562501313 ) ) ;
#29826=CARTESIAN_POINT ( 'NONE',  ( 4.508719565894415915, 1.847421675581904843, -60.89141554682500157 ) ) ;
#29845=CARTESIAN_POINT ( 'NONE',  ( 1.894269134907880847, -4.501889487458040406, -44.10000000002499121 ) ) ;
#29852=CARTESIAN_POINT ( 'NONE',  ( 5.200437648300224147, 1.853818095060352222, -45.12627377572500365 ) ) ;
#29866=CARTESIAN_POINT ( 'NONE',  ( 5.363076718300177959, -2.525690298526013677, -52.77872167392499847 ) ) ;
#29913=( NAMED_UNIT ( * ) SI_UNIT ( $, .STERADIAN. ) SOLID_ANGLE_UNIT ( ) );
#29924=CARTESIAN_POINT ( 'NONE',  ( -4.072259770650453525, 2.021700601781290629, -57.19877225282498756 ) ) ;
#29937=CARTESIAN_POINT ( 'NONE',  ( 1.169850847344618083, -6.301966510834352775, -58.74125695792500323 ) ) ;
#29943=CARTESIAN_POINT ( 'NONE',  ( -4.162561055638823504, 0.1692103760920289357, -68.10000000002501963 ) ) ;
#29952=CARTESIAN_POINT ( 'NONE',  ( -5.427432314178970429, 2.515719109140460041, -65.77526299442500601 ) ) ;
#29969=CARTESIAN_POINT ( 'NONE',  ( -4.216190498783925378, -2.983089501615236561, -44.28462724592499455 ) ) ;
#29976=CARTESIAN_POINT ( 'NONE',  ( 0.4806848194628341453, -3.969394140205261490, -68.10000000002499121 ) ) ;
#29981=CARTESIAN_POINT ( 'NONE',  ( 1.387947292976095426, 4.364053279572889465, -60.86492395752500784 ) ) ;
#30007=CARTESIAN_POINT ( 'NONE',  ( 4.545032752014871669, -0.3361547907463971474, -49.12442242802499237 ) ) ;
#30021=CARTESIAN_POINT ( 'NONE',  ( 4.101176313917077820, -1.931410228222282921, -52.29872167392500160 ) ) ;
#30097=CARTESIAN_POINT ( 'NONE',  ( 4.003591150705129387, -2.204345408526039218, -58.30843849682500490 ) ) ;
#30115=CARTESIAN_POINT ( 'NONE',  ( -3.112296099710462727, 3.758517760630103233, -62.99933298492499034 ) ) ;
#30138=CARTESIAN_POINT ( 'NONE',  ( 2.235634928214019990, -3.593586099038730275, -68.10000000002501963 ) ) ;
#30141=CARTESIAN_POINT ( 'NONE',  ( -4.194654192376331636, 0.4516430622356696900, -44.10000000002499831 ) ) ;
#30145=CARTESIAN_POINT ( 'NONE',  ( 2.833778097863423717, 3.583098331959791771, -64.03768011632499224 ) ) ;
#30159=CARTESIAN_POINT ( 'NONE',  ( -0.5400457538399249247, -3.901550194262492610, -44.10000000002499121 ) ) ;
#30169=CARTESIAN_POINT ( 'NONE',  ( 4.432674687120906398, 4.607520344841867121, -48.69426496242499525 ) ) ;
#30181=CARTESIAN_POINT ( 'NONE',  ( 4.692739937114380311, 0.5303478879429834869, -55.01771407622499765 ) ) ;
#30253=CARTESIAN_POINT ( 'NONE',  ( 1.815007998551255941, 5.706838904126064094, -60.46492395752500215 ) ) ;
#30272=CARTESIAN_POINT ( 'NONE',  ( -4.475180390489594373, -2.644424941261572126, -67.57382590962500046 ) ) ;
#30299=CARTESIAN_POINT ( 'NONE',  ( 2.566301578609887279, -3.483224111942909040, -68.10000000002499121 ) ) ;
#30301=CARTESIAN_POINT ( 'NONE',  ( -4.278771218549574762, 1.040277833517747164, -44.10000000002499121 ) ) ;
#30306=CARTESIAN_POINT ( 'NONE',  ( -5.427432314178970429, 2.515719109140460041, -65.77526299442500601 ) ) ;
#30335=CARTESIAN_POINT ( 'NONE',  ( -5.473571180597741836, 3.247285761689575168, -50.35267869292499654 ) ) ;
#30345=CARTESIAN_POINT ( 'NONE',  ( -3.882843611323257615, 4.424263292022076577, -54.78587006832498219 ) ) ;
#30388=CARTESIAN_POINT ( 'NONE',  ( 3.248659393266396300, -2.157825791482658850, -43.75875473022500728 ) ) ;
#30421=CARTESIAN_POINT ( 'NONE',  ( -1.494970809075166329, -6.161113191638062148, -61.94311227092499195 ) ) ;
#30431=CARTESIAN_POINT ( 'NONE',  ( -2.098441946322436635, -3.287561928151557122, -68.10000000002500542 ) ) ;
#30434=ORIENTED_EDGE ( 'NONE', *, *, #30577, .F. ) ;
#30440=CARTESIAN_POINT ( 'NONE',  ( 4.117846205589234643, 1.989599136607407504, -66.85315453642499506 ) ) ;
#30458=CARTESIAN_POINT ( 'NONE',  ( -2.158984558600606007, 5.217364672555318883, -57.14652090042499566 ) ) ;
#30464=CARTESIAN_POINT ( 'NONE',  ( 1.201297883400354261, -3.884613871942808050, -68.10000000002501963 ) ) ;
#30467=CARTESIAN_POINT ( 'NONE',  ( -4.335682707025502403, 1.120073662811198689, -44.10000000002499121 ) ) ;
#30471=CARTESIAN_POINT ( 'NONE',  ( 1.082264403401735020, -4.420062499635217357, -64.70397119102501904 ) ) ;
#30498=CARTESIAN_POINT ( 'NONE',  ( -0.7556487780321572423, 4.453147011089724217, -51.25792092402500089 ) ) ;
#30506=CARTESIAN_POINT ( 'NONE',  ( 2.752605500610148859, 3.655072764496607007, -54.62619010302499589 ) ) ;
#30574=CARTESIAN_POINT ( 'NONE',  ( -4.240613917342964889, -1.711409762446096439, -58.98491726642500055 ) ) ;
#30577=EDGE_CURVE ( 'NONE', #29133, #1473, #5067, .T. ) ;
#30592=CARTESIAN_POINT ( 'NONE',  ( -4.617404660156336327, 1.522451704138575668, -67.99019511502500279 ) ) ;
#30614=CARTESIAN_POINT ( 'NONE',  ( -1.293561172433232986, -6.216321778783836294, -52.92706695232499925 ) ) ;
#30621=CARTESIAN_POINT ( 'NONE',  ( 2.743523579834141746, -3.445032478160675371, -68.10000000002501963 ) ) ;
#30624=CARTESIAN_POINT ( 'NONE',  ( -4.094000917768401138, -0.2590052599951323531, -44.10000000002498410 ) ) ;
#30627=CARTESIAN_POINT ( 'NONE',  ( 1.415268835064556363, -5.780081730213937341, -64.70397119102500483 ) ) ;
#30652=CARTESIAN_POINT ( 'NONE',  ( 5.782578939028539367, 2.564649547393091478, -51.87998794302499306 ) ) ;
#30662=CARTESIAN_POINT ( 'NONE',  ( -5.939015604524707115, -0.1501891088408410790, -53.55673954922500002 ) ) ;
#30694=CARTESIAN_POINT ( 'NONE',  ( -5.162912894389027230, 3.035924517800103750, -45.32354844312499864 ) ) ;
#30725=CARTESIAN_POINT ( 'NONE',  ( -0.8884012486115674401, 4.851036559086118416, -59.50324387862499265 ) ) ;
#30738=CARTESIAN_POINT ( 'NONE',  ( -5.167095691178253070, 1.703695954683749125, -67.94019511502500563 ) ) ;
#30766=CARTESIAN_POINT ( 'NONE',  ( 2.707138150663993326, -3.848833623503777446, -68.10000000002500542 ) ) ;
#30769=CARTESIAN_POINT ( 'NONE',  ( -4.734981018114883256, 0.5816554918100906857, -44.10000000002498410 ) ) ;
#30773=CARTESIAN_POINT ( 'NONE',  ( 3.225090657556859419, -3.689912930009636938, -65.24605006312501132 ) ) ;
#30778=CARTESIAN_POINT ( 'NONE',  ( -2.098672137722010334, -3.287437779826620776, -44.10000000002499121 ) ) ;
#30799=CARTESIAN_POINT ( 'NONE',  ( 5.053719932302922935, 0.5711438793038403627, -54.26771407622499765 ) ) ;
#30809=CARTESIAN_POINT ( 'NONE',  ( -5.473210459068893918, -0.1384095709066185120, -54.35673954922499718 ) ) ;
#30835=CARTESIAN_POINT ( 'NONE',  ( -1.557622931652909104, -4.259165208650869339, -43.98640794712500224 ) ) ;
#30849=CARTESIAN_POINT ( 'NONE',  ( 0.5921542527409766610, -4.847825725916151463, -44.53057807742500529 ) ) ;
#30900=CARTESIAN_POINT ( 'NONE',  ( 2.708949881112989289, 3.684664522020659305, -66.24226422532500180 ) ) ;
#30918=CARTESIAN_POINT ( 'NONE',  ( 5.762915210551160072, -2.052471225477275674, -67.23341453912500754 ) ) ;
#30927=CARTESIAN_POINT ( 'NONE',  ( -4.792751602502305808, 0.3708384435674089152, -68.10000000002500542 ) ) ;
#30934=CARTESIAN_POINT ( 'NONE',  ( 0.2444022557069348567, 3.892334458579129297, -69.75875473022499307 ) ) ;
#30937=CARTESIAN_POINT ( 'NONE',  ( -4.072259770650454413, 2.021700601781299511, -56.79877225282499609 ) ) ;
#30956=CARTESIAN_POINT ( 'NONE',  ( -0.9891938378274514054, -4.753657830815118501, -52.52706695232500067 ) ) ;
#30965=CARTESIAN_POINT ( 'NONE',  ( -3.855177830964256813, -4.571422008809257420, -59.17407541852499975 ) ) ;
#30989=CARTESIAN_POINT ( 'NONE',  ( 0.5921542527520354815, -4.847825725899490124, -43.03057807742499818 ) ) ;
#31069=CARTESIAN_POINT ( 'NONE',  ( -3.807105672873282831, -5.136256491778199873, -65.13409070562501313 ) ) ;
#31089=CARTESIAN_POINT ( 'NONE',  ( -3.112296099710462727, 3.758517760630103233, -62.99933298492499034 ) ) ;
ENDSEC;
END-ISO-10303-21;
